ISO-10303-21;
HEADER;
FILE_DESCRIPTION (('STEP AP214'),
    '1' );
FILE_NAME ('Snap Open Cable Crossbars 5.step',
    '2026-10-08T22:59:04',
    ( '' ),
    ( '' ),
    'SwSTEP 2.0',
    'SolidWorks 2020',
    '' );
FILE_SCHEMA (( 'AUTOMOTIVE_DESIGN' ));
ENDSEC;

DATA;
#25=ADVANCED_FACE ( 'NONE', ( #203377 ), #234826, .T. ) ;
#221=VERTEX_POINT ( 'NONE', #213632 ) ;
#249=LINE ( 'NONE', #242710, #54314 ) ;
#383=ORIENTED_EDGE ( 'NONE', *, *, #120416, .F. ) ;
#557=CARTESIAN_POINT ( 'NONE',  ( 16.87683809663750267, 9.950000000011138823, -146.6500000000000341 ) ) ;
#693=LINE ( 'NONE', #254979, #156291 ) ;
#715=CARTESIAN_POINT ( 'NONE',  ( -16.87683809663752399, 21.23804903844422043, -146.6500000000000341 ) ) ;
#1028=VERTEX_POINT ( 'NONE', #117468 ) ;
#1158=LINE ( 'NONE', #121168, #231032 ) ;
#1241=CARTESIAN_POINT ( 'NONE',  ( -16.88495309932523369, 9.954627058484017965, -146.6345486738119348 ) ) ;
#1366=VERTEX_POINT ( 'NONE', #174615 ) ;
#1521=CARTESIAN_POINT ( 'NONE',  ( -17.04761207306821191, 10.02645087340893326, -146.6500000000000341 ) ) ;
#1522=CARTESIAN_POINT ( 'NONE',  ( -17.80356949363962826, 10.87673139701326441, -157.2130730242256220 ) ) ;
#1612=FACE_OUTER_BOUND ( 'NONE', #57645, .T. ) ;
#1696=AXIS2_PLACEMENT_3D ( 'NONE', #2027, #103687, #241933 ) ;
#1885=LINE ( 'NONE', #158448, #203915 ) ;
#2027=CARTESIAN_POINT ( 'NONE',  ( 20.04999999999999716, 8.750000000011173285, -143.2500000000000284 ) ) ;
#2300=ORIENTED_EDGE ( 'NONE', *, *, #78334, .T. ) ;
#2425=AXIS2_PLACEMENT_3D ( 'NONE', #153513, #135160, #16531 ) ;
#2547=B_SPLINE_CURVE_WITH_KNOTS ( 'NONE', 3,
 ( #96098, #113115, #135226, #115685, #231794, #195248, #14028, #92254, #32325, #250060, #133949, #71442, #51832, #111841, #233089, #175670, #212235, #230501, #251326, #131387, #153577, #191402, #173141, #213490, #36162, #54419 ),
 .UNSPECIFIED., .F., .F.,
 ( 4, 2, 2, 2, 2, 2, 2, 2, 2, 2, 2, 2, 4 ),
 ( 0.005476422646581349113, 0.006160811967703589548, 0.006845201288825829983, 0.007187395949386920710, 0.007529590609948011437, 0.007871785270509102164, 0.008213979931070192891, 0.008556174591631285353, 0.008898369252192376080, 0.009240563912753466808, 0.009582758573314557535, 0.01026714789443679797, 0.01095153721555903840 ),
 .UNSPECIFIED. ) ;
#2726=EDGE_CURVE ( 'NONE', #168716, #81862, #139119, .T. ) ;
#2784=PLANE ( 'NONE',  #133343 ) ;
#2801=CARTESIAN_POINT ( 'NONE',  ( 20.27550659511088682, 9.216043722520002035, -143.2500000000000284 ) ) ;
#2854=AXIS2_PLACEMENT_3D ( 'NONE', #174416, #153568, #135216 ) ;
#3118=CARTESIAN_POINT ( 'NONE',  ( 18.54999999999999716, 23.65833333334447985, -150.7500000000000284 ) ) ;
#3188=CARTESIAN_POINT ( 'NONE',  ( -13.11924609551136456, 9.431689550535260480, -152.2792900322361049 ) ) ;
#3396=CARTESIAN_POINT ( 'NONE',  ( 13.77030915526559340, 9.456007326080465347, -152.4886334941467965 ) ) ;
#3428=CARTESIAN_POINT ( 'NONE',  ( 20.09999999999999787, 9.750000000011137757, -154.8500000000000227 ) ) ;
#3479=DIRECTION ( 'NONE',  ( -1.000000000000000000, 0.000000000000000000, 0.000000000000000000 ) ) ;
#3577=ADVANCED_FACE ( 'NONE', ( #214129 ), #171191, .F. ) ;
#3956=CARTESIAN_POINT ( 'NONE',  ( 20.73486653747088582, 7.250000000011182166, -143.2500000000000284 ) ) ;
#4058=DIRECTION ( 'NONE',  ( -1.000000000000000000, 0.000000000000000000, 0.000000000000000000 ) ) ;
#4270=DIRECTION ( 'NONE',  ( 0.000000000000000000, 1.000000000000000000, 0.000000000000000000 ) ) ;
#4342=EDGE_CURVE ( 'NONE', #56249, #236861, #91948, .T. ) ;
#4363=CARTESIAN_POINT ( 'NONE',  ( -18.39999999999999858, 11.47316190337362762, -143.3259460668079726 ) ) ;
#4436=DIRECTION ( 'NONE',  ( 0.000000000000000000, 0.000000000000000000, 1.000000000000000000 ) ) ;
#4482=CARTESIAN_POINT ( 'NONE',  ( -14.56336952470180535, 9.446645344706400493, -152.4108064561002607 ) ) ;
#4515=LINE ( 'NONE', #204009, #149005 ) ;
#4527=VECTOR ( 'NONE', #115219, 1000.000000000000000 ) ;
#4528=ORIENTED_EDGE ( 'NONE', *, *, #129617, .T. ) ;
#4614=DIRECTION ( 'NONE',  ( 1.000000000000000000, -0.000000000000000000, -0.000000000000000000 ) ) ;
#4896=CARTESIAN_POINT ( 'NONE',  ( -16.94309007106720699, 9.992226192581142641, -146.6057912825555150 ) ) ;
#5244=EDGE_LOOP ( 'NONE', ( #218896, #68781, #179464, #128259, #210819 ) ) ;
#5296=CARTESIAN_POINT ( 'NONE',  ( -17.01764560440334151, 9.950000000011138823, -146.7499999992111270 ) ) ;
#5345=CARTESIAN_POINT ( 'NONE',  ( 14.87567385445976953, 9.430764995433476017, -149.2305373947504847 ) ) ;
#5387=DIRECTION ( 'NONE',  ( 1.000000000000000000, 0.000000000000000000, 0.000000000000000000 ) ) ;
#5521=ADVANCED_FACE ( 'NONE', ( #41032 ), #100926, .F. ) ;
#5552=VERTEX_POINT ( 'NONE', #125677 ) ;
#5594=AXIS2_PLACEMENT_3D ( 'NONE', #19810, #141034, #40682 ) ;
#5754=CARTESIAN_POINT ( 'NONE',  ( -13.77083647240106501, 9.457410930301316299, -152.4999159087463170 ) ) ;
#5767=CARTESIAN_POINT ( 'NONE',  ( 20.05000000000002913, 7.250000000011171508, -143.2500000000000284 ) ) ;
#5782=CARTESIAN_POINT ( 'NONE',  ( -16.81744102076748959, 9.950000000011138823, -154.8500000000000227 ) ) ;
#5958=CARTESIAN_POINT ( 'NONE',  ( 15.51872946208854920, 9.376580978055097049, -151.6269462470119720 ) ) ;
#6345=AXIS2_PLACEMENT_3D ( 'NONE', #64875, #166581, #66167 ) ;
#6664=CARTESIAN_POINT ( 'NONE',  ( -18.34374000495060386, 11.47316190337362585, -143.2500000000000284 ) ) ;
#6767=CARTESIAN_POINT ( 'NONE',  ( -16.85722902420155478, 9.950000000011137047, -146.7655474737703685 ) ) ;
#7029=VERTEX_POINT ( 'NONE', #207722 ) ;
#7248=ORIENTED_EDGE ( 'NONE', *, *, #16628, .F. ) ;
#7250=CARTESIAN_POINT ( 'NONE',  ( 13.88638282980484462, 9.457426452500058645, -152.5000418684000749 ) ) ;
#7252=B_SPLINE_CURVE_WITH_KNOTS ( 'NONE', 3,
 ( #65958, #243294, #103769, #125915, #145485, #184613, #5958, #85476, #205451, #146742, #102479, #26860, #106338, #7250, #3396, #204165, #185898, #162509, #25560, #62114, #86782, #187210, #127217, #107646, #43832, #141637, #223727, #142896, #88054, #202896 ),
 .UNSPECIFIED., .F., .F.,
 ( 4, 2, 2, 2, 2, 2, 2, 2, 2, 2, 2, 2, 2, 2, 4 ),
 ( 0.000000000000000000, 0.0003422764154113113887, 0.0006845528308226227774, 0.001026829246233936172, 0.001369105661645249458, 0.002053658492467934794, 0.002738211323290619913, 0.003080487738701959653, 0.003422764154113299394, 0.003765040569524640002, 0.004107316984935979742, 0.004449593400347319483, 0.004791869815758659223, 0.005134146231169999831, 0.005476422646581339572 ),
 .UNSPECIFIED. ) ;
#7317=CARTESIAN_POINT ( 'NONE',  ( 18.54999999999999716, 8.750000000011173285, -146.6500000000000341 ) ) ;
#7421=ORIENTED_EDGE ( 'NONE', *, *, #196813, .T. ) ;
#7423=CARTESIAN_POINT ( 'NONE',  ( -16.87683809663752399, 9.864913447291341342, -154.2242815513039318 ) ) ;
#7519=CARTESIAN_POINT ( 'NONE',  ( 13.99999999999999822, 9.850000000011137402, -150.7500000000000284 ) ) ;
#7535=ORIENTED_EDGE ( 'NONE', *, *, #246377, .F. ) ;
#7557=DIRECTION ( 'NONE',  ( 1.000000000000000000, -0.000000000000000000, -0.000000000000000000 ) ) ;
#7615=ORIENTED_EDGE ( 'NONE', *, *, #155134, .T. ) ;
#7741=CARTESIAN_POINT ( 'NONE',  ( -18.35235881385853318, 11.47341900772405054, -143.2500000000000284 ) ) ;
#7766=ADVANCED_FACE ( 'NONE', ( #200685 ), #144536, .F. ) ;
#7828=ORIENTED_EDGE ( 'NONE', *, *, #54871, .T. ) ;
#8047=DIRECTION ( 'NONE',  ( -1.000000000000000000, 0.000000000000000000, 0.000000000000000000 ) ) ;
#8194=CARTESIAN_POINT ( 'NONE',  ( -16.87683809663752399, 9.950000000011142376, -146.6500000000000341 ) ) ;
#8490=EDGE_CURVE ( 'NONE', #11462, #149588, #249317, .T. ) ;
#8540=VECTOR ( 'NONE', #11262, 1000.000000000000000 ) ;
#8624=EDGE_CURVE ( 'NONE', #118840, #171058, #136872, .T. ) ;
#8635=ADVANCED_FACE ( 'NONE', ( #146483 ), #228627, .F. ) ;
#9073=EDGE_LOOP ( 'NONE', ( #187388, #75847, #24826, #154724, #207541, #171355 ) ) ;
#9161=EDGE_LOOP ( 'NONE', ( #63328, #161217, #196096, #47365 ) ) ;
#9174=ORIENTED_EDGE ( 'NONE', *, *, #111877, .T. ) ;
#9223=VERTEX_POINT ( 'NONE', #256460 ) ;
#9357=CARTESIAN_POINT ( 'NONE',  ( -16.89268316805465986, 9.951721813253337601, -154.8557524785455541 ) ) ;
#9362=ADVANCED_FACE ( 'NONE', ( #102551 ), #165136, .F. ) ;
#9447=CARTESIAN_POINT ( 'NONE',  ( -23.25000000000000355, 5.650000000011139001, -154.8500000000000227 ) ) ;
#9647=DIRECTION ( 'NONE',  ( -1.000000000000000000, 0.000000000000000000, 0.000000000000000000 ) ) ;
#9689=CARTESIAN_POINT ( 'NONE',  ( 23.24999999999999645, 11.75000000001113953, -143.2500000000000284 ) ) ;
#9857=LINE ( 'NONE', #172837, #95288 ) ;
#9959=PLANE ( 'NONE',  #93854 ) ;
#9972=AXIS2_PLACEMENT_3D ( 'NONE', #113067, #72683, #156074 ) ;
#9992=CARTESIAN_POINT ( 'NONE',  ( 18.39999999999997371, 11.47316190337362940, -158.2500000000000284 ) ) ;
#10139=VERTEX_POINT ( 'NONE', #247820 ) ;
#10223=LINE ( 'NONE', #89730, #175974 ) ;
#10838=CARTESIAN_POINT ( 'NONE',  ( -16.86733706339143168, 9.965990529650822438, -154.9031153019987244 ) ) ;
#11224=EDGE_CURVE ( 'NONE', #254838, #62456, #38343, .T. ) ;
#11262=DIRECTION ( 'NONE',  ( -0.7071067811865456854, 0.7071067811865493491, 0.000000000000000000 ) ) ;
#11462=VERTEX_POINT ( 'NONE', #256785 ) ;
#11705=VERTEX_POINT ( 'NONE', #63776 ) ;
#11720=DIRECTION ( 'NONE',  ( -1.000000000000000000, 1.652117596168391700E-15, 0.000000000000000000 ) ) ;
#11738=EDGE_CURVE ( 'NONE', #199264, #115602, #169341, .T. ) ;
#11914=CARTESIAN_POINT ( 'NONE',  ( -16.94878442675512531, 9.991729103002162660, -146.6117804243621379 ) ) ;
#11977=CARTESIAN_POINT ( 'NONE',  ( 21.72449340488910252, 10.28395627750227703, -146.6500000000000341 ) ) ;
#12056=LINE ( 'NONE', #168591, #55975 ) ;
#12145=CARTESIAN_POINT ( 'NONE',  ( -16.86420534634261514, 9.970615445602874161, -154.9183365492374094 ) ) ;
#12525=ORIENTED_EDGE ( 'NONE', *, *, #212637, .T. ) ;
#12584=DIRECTION ( 'NONE',  ( -0.5932847527679298016, 0.8049926720990051576, 0.000000000000000000 ) ) ;
#13043=CARTESIAN_POINT ( 'NONE',  ( -16.94107738177415712, 10.01423928514777728, -146.5500000000000114 ) ) ;
#13182=CARTESIAN_POINT ( 'NONE',  ( -16.89318236219976299, 9.951535257886295227, -146.6448703678941285 ) ) ;
#13183=VECTOR ( 'NONE', #103183, 1000.000000000000000 ) ;
#13246=CARTESIAN_POINT ( 'NONE',  ( -18.40000000000000213, 5.650000000011139001, -154.8500000000000227 ) ) ;
#13274=VECTOR ( 'NONE', #235965, 1000.000000000000000 ) ;
#13280=CARTESIAN_POINT ( 'NONE',  ( -16.93294127766158752, 10.00328010296601988, -154.9299072658292573 ) ) ;
#13304=DIRECTION ( 'NONE',  ( -1.020425574104004196E-15, 0.000000000000000000, -1.000000000000000000 ) ) ;
#13372=VECTOR ( 'NONE', #34567, 1000.000000000000000 ) ;
#13540=ORIENTED_EDGE ( 'NONE', *, *, #189760, .T. ) ;
#13821=UNCERTAINTY_MEASURE_WITH_UNIT (LENGTH_MEASURE( 1.000000000000000082E-05 ), #120776, 'distance_accuracy_value', 'NONE');
#13872=VECTOR ( 'NONE', #253233, 1000.000000000000000 ) ;
#14028=CARTESIAN_POINT ( 'NONE',  ( -15.06774609480955363, 9.417651958852161442, -149.3587873924404619 ) ) ;
#14164=DIRECTION ( 'NONE',  ( 0.7071067811865456854, -0.7071067811865493491, -0.000000000000000000 ) ) ;
#14414=VECTOR ( 'NONE', #9647, 1000.000000000000000 ) ;
#14544=ORIENTED_EDGE ( 'NONE', *, *, #53617, .F. ) ;
#14570=B_SPLINE_CURVE_WITH_KNOTS ( 'NONE', 3,
 ( #31712, #53810, #111216, #228612, #10838, #12145, #89070, #90354, #154243, #192060 ),
 .UNSPECIFIED., .F., .F.,
 ( 4, 3, 3, 4 ),
 ( 7.632826238681696029E-06, 4.756916949875625587E-05, 9.484459048152062838E-05, 0.0001435500935100044199 ),
 .UNSPECIFIED. ) ;
#14662=LINE ( 'NONE', #61140, #63222 ) ;
#14688=AXIS2_PLACEMENT_3D ( 'NONE', #223675, #183286, #63320 ) ;
#14769=CARTESIAN_POINT ( 'NONE',  ( -17.11825945287481332, 9.950000000011138823, -154.7500000000000284 ) ) ;
#14835=DIRECTION ( 'NONE',  ( -0.000000000000000000, -0.000000000000000000, -1.000000000000000000 ) ) ;
#14892=PLANE ( 'NONE',  #199409 ) ;
#15169=ORIENTED_EDGE ( 'NONE', *, *, #129776, .F. ) ;
#15618=CARTESIAN_POINT ( 'NONE',  ( -16.77732147262506146, 9.945966932629788815, -154.8364912432759013 ) ) ;
#15620=FACE_OUTER_BOUND ( 'NONE', #245586, .T. ) ;
#15723=AXIS2_PLACEMENT_3D ( 'NONE', #188221, #69574, #231221 ) ;
#15960=CARTESIAN_POINT ( 'NONE',  ( 18.39999999999999503, 11.75000000001113953, -146.6500000000000341 ) ) ;
#16098=LINE ( 'NONE', #175194, #88174 ) ;
#16261=CARTESIAN_POINT ( 'NONE',  ( -16.97683810757273193, 9.950000000011137047, -154.2364232875389121 ) ) ;
#16531=DIRECTION ( 'NONE',  ( 1.000000000000000000, 0.000000000000000000, 0.000000000000000000 ) ) ;
#16628=EDGE_CURVE ( 'NONE', #143978, #107290, #229153, .T. ) ;
#16675=DIRECTION ( 'NONE',  ( 1.073024830501117725E-15, 0.000000000000000000, 1.000000000000000000 ) ) ;
#16729=DIRECTION ( 'NONE',  ( 1.000000000000000000, 0.000000000000000000, 0.000000000000000000 ) ) ;
#16933=FACE_OUTER_BOUND ( 'NONE', #126493, .T. ) ;
#17111=CARTESIAN_POINT ( 'NONE',  ( -18.39418127959864790, 11.48390560170929220, -158.2500000000000284 ) ) ;
#17125=ORIENTED_EDGE ( 'NONE', *, *, #145596, .T. ) ;
#17133=DIRECTION ( 'NONE',  ( -1.073024830501117725E-15, 0.000000000000000000, 1.000000000000000000 ) ) ;
#17172=ORIENTED_EDGE ( 'NONE', *, *, #250428, .T. ) ;
#17241=VECTOR ( 'NONE', #140400, 1000.000000000000000 ) ;
#17278=AXIS2_PLACEMENT_3D ( 'NONE', #181476, #41968, #39411 ) ;
#17347=CARTESIAN_POINT ( 'NONE',  ( -16.84421487269769102, 9.950000000011135270, -146.6695021224449533 ) ) ;
#17519=FACE_OUTER_BOUND ( 'NONE', #71324, .T. ) ;
#17723=DIRECTION ( 'NONE',  ( -1.186688945009010077E-16, 1.000000000000000000, 0.000000000000000000 ) ) ;
#17734=AXIS2_PLACEMENT_3D ( 'NONE', #165823, #163246, #64136 ) ;
#18244=CARTESIAN_POINT ( 'NONE',  ( 20.27550659511088682, 9.216043722520002035, -143.2500000000000284 ) ) ;
#18261=CARTESIAN_POINT ( 'NONE',  ( -16.87845715379269507, 9.957858113908169884, -146.6238006510589287 ) ) ;
#18905=CARTESIAN_POINT ( 'NONE',  ( -17.01764560440359730, 9.950000000011138823, -154.7500000007889298 ) ) ;
#19192=CARTESIAN_POINT ( 'NONE',  ( -16.80438519320023616, 9.949779096479501206, -146.6507382809213027 ) ) ;
#19364=ORIENTED_EDGE ( 'NONE', *, *, #223145, .T. ) ;
#19618=ORIENTED_EDGE ( 'NONE', *, *, #127837, .F. ) ;
#19810=CARTESIAN_POINT ( 'NONE',  ( -14.00000000000000178, 9.850000000011133849, -150.7500000000000284 ) ) ;
#20150=DIRECTION ( 'NONE',  ( -1.000000000000000000, -1.186688945009010077E-16, -0.000000000000000000 ) ) ;
#20210=CARTESIAN_POINT ( 'NONE',  ( -17.11825945287481687, 10.05000000001113847, -154.8500000000000227 ) ) ;
#20219=CARTESIAN_POINT ( 'NONE',  ( -15.06720934482786056, 9.417690691074257714, -152.1416006967646695 ) ) ;
#20850=DIRECTION ( 'NONE',  ( 1.000000000000000000, 0.000000000000000000, 0.000000000000000000 ) ) ;
#20910=CARTESIAN_POINT ( 'NONE',  ( -16.94878442675512886, 9.991729103002160883, -154.8882195756378906 ) ) ;
#21226=CARTESIAN_POINT ( 'NONE',  ( -23.25000000000000355, 11.75000000001113953, -143.2500000000000284 ) ) ;
#21367=ADVANCED_FACE ( 'NONE', ( #211797 ), #14892, .T. ) ;
#21369=ORIENTED_EDGE ( 'NONE', *, *, #156647, .F. ) ;
#21457=LINE ( 'NONE', #98354, #22247 ) ;
#21523=ORIENTED_EDGE ( 'NONE', *, *, #79968, .F. ) ;
#21553=AXIS2_PLACEMENT_3D ( 'NONE', #26251, #245293, #27562 ) ;
#21623=FACE_OUTER_BOUND ( 'NONE', #229291, .T. ) ;
#21654=CARTESIAN_POINT ( 'NONE',  ( -16.88815647973234135, 9.950832619326892114, -146.6472170633260248 ) ) ;
#22247=VECTOR ( 'NONE', #200076, 1000.000000000000000 ) ;
#22565=VERTEX_POINT ( 'NONE', #160366 ) ;
#22672=ORIENTED_EDGE ( 'NONE', *, *, #82560, .F. ) ;
#22833=CARTESIAN_POINT ( 'NONE',  ( -16.87372386987899375, 9.880600233647912845, -147.1492698718664940 ) ) ;
#22897=PLANE ( 'NONE',  #33928 ) ;
#22957=CARTESIAN_POINT ( 'NONE',  ( -16.87851181299898329, 9.950042924018893231, -146.6498564846331192 ) ) ;
#23069=CARTESIAN_POINT ( 'NONE',  ( -16.77977881697927032, 9.946601933544062746, -146.6613785731150585 ) ) ;
#23091=ORIENTED_EDGE ( 'NONE', *, *, #81305, .F. ) ;
#23174=CARTESIAN_POINT ( 'NONE',  ( -16.81453563122428818, 9.939100205448108127, -154.7882586606453401 ) ) ;
#23437=EDGE_CURVE ( 'NONE', #203363, #31535, #58755, .T. ) ;
#23563=EDGE_CURVE ( 'NONE', #221934, #226856, #108736, .T. ) ;
#23667=VERTEX_POINT ( 'NONE', #100369 ) ;
#23799=CARTESIAN_POINT ( 'NONE',  ( -16.77431908686106254, 9.945805754529134290, -146.6641607823497964 ) ) ;
#24086=CARTESIAN_POINT ( 'NONE',  ( -15.15564720441980207, 9.410708747058237122, -152.0692084058441367 ) ) ;
#24128=DIRECTION ( 'NONE',  ( 0.000000000000000000, 0.000000000000000000, -1.000000000000000000 ) ) ;
#24217=EDGE_CURVE ( 'NONE', #221299, #156630, #94014, .T. ) ;
#24239=ORIENTED_EDGE ( 'NONE', *, *, #115787, .T. ) ;
#24486=B_SPLINE_CURVE_WITH_KNOTS ( 'NONE', 3,
 ( #219838, #200287, #21654, #101121, #180731, #22957, #63322, #222377, #85427, #243246 ),
 .UNSPECIFIED., .F., .F.,
 ( 4, 3, 3, 4 ),
 ( 1.950915401637565782E-15, 8.145022132839031210E-06, 1.905645951092651034E-05, 2.061107371226032482E-05 ),
 .UNSPECIFIED. ) ;
#24590=ORIENTED_EDGE ( 'NONE', *, *, #147256, .F. ) ;
#24718=LINE ( 'NONE', #147197, #211942 ) ;
#24766=CARTESIAN_POINT ( 'NONE',  ( -16.87036670365548474, 9.989418819312801290, -154.9795601173020714 ) ) ;
#24798=ORIENTED_EDGE ( 'NONE', *, *, #165273, .F. ) ;
#24814=ORIENTED_EDGE ( 'NONE', *, *, #214868, .F. ) ;
#24826=ORIENTED_EDGE ( 'NONE', *, *, #150147, .T. ) ;
#24873=DIRECTION ( 'NONE',  ( -1.073024830501117725E-15, 0.000000000000000000, 1.000000000000000000 ) ) ;
#25136=ORIENTED_EDGE ( 'NONE', *, *, #155118, .T. ) ;
#25245=CARTESIAN_POINT ( 'NONE',  ( -18.40000000000000213, 11.48667500176882328, -143.2500000000000284 ) ) ;
#25398=DIRECTION ( 'NONE',  ( 1.000000000000000000, 0.000000000000000000, 1.073024830501117725E-15 ) ) ;
#25449=DIRECTION ( 'NONE',  ( 0.000000000000000000, 0.000000000000000000, 1.000000000000000000 ) ) ;
#25560=CARTESIAN_POINT ( 'NONE',  ( 13.12229106158772218, 9.430637101707896264, -152.2682606180609639 ) ) ;
#25660=CARTESIAN_POINT ( 'NONE',  ( 18.39999999999999503, 5.650000000011139001, -146.6500000000000341 ) ) ;
#26217=VECTOR ( 'NONE', #74979, 1000.000000000000000 ) ;
#26251=CARTESIAN_POINT ( 'NONE',  ( 18.54999999999999716, 8.750000000011182166, -143.2500000000000284 ) ) ;
#26374=VECTOR ( 'NONE', #147160, 1000.000000000000000 ) ;
#26688=PLANE ( 'NONE',  #97783 ) ;
#26744=PLANE ( 'NONE',  #237961 ) ;
#26795=CARTESIAN_POINT ( 'NONE',  ( -17.04761207306819770, 10.02645087340893149, -154.8500000000000512 ) ) ;
#26837=EDGE_CURVE ( 'NONE', #217779, #67383, #167421, .T. ) ;
#26860=CARTESIAN_POINT ( 'NONE',  ( 14.45963434102924694, 9.451541661396669625, -152.4538754988305982 ) ) ;
#26864=EDGE_LOOP ( 'NONE', ( #160576, #197352, #91400, #128655 ) ) ;
#26921=ADVANCED_FACE ( 'NONE', ( #52570 ), #48722, .F. ) ;
#27078=CARTESIAN_POINT ( 'NONE',  ( -16.92132318717937522, 9.966070024017081863, -146.6224066303520885 ) ) ;
#27123=ORIENTED_EDGE ( 'NONE', *, *, #179764, .F. ) ;
#27228=EDGE_LOOP ( 'NONE', ( #234782, #65753, #23091 ) ) ;
#27551=CARTESIAN_POINT ( 'NONE',  ( 14.11444803880197085, 9.457431528860068326, -148.9999169378996555 ) ) ;
#27562=DIRECTION ( 'NONE',  ( 0.000000000000000000, 0.000000000000000000, -1.000000000000000000 ) ) ;
#27836=ORIENTED_EDGE ( 'NONE', *, *, #224172, .T. ) ;
#28128=( BOUNDED_CURVE ( )  B_SPLINE_CURVE ( 3, ( #256003, #99522, #77402, #257287 ),
 .UNSPECIFIED., .F., .F. ) 
 B_SPLINE_CURVE_WITH_KNOTS ( ( 4, 4 ),
 ( 0.3000847527772385614, 0.5517402753107881752 ),
 .UNSPECIFIED. ) 
 CURVE ( )  GEOMETRIC_REPRESENTATION_ITEM ( )  RATIONAL_B_SPLINE_CURVE ( ( 1.000000000000000000, 0.9947294176030464508, 0.9947294176030464508, 1.000000000000000000 ) ) 
 REPRESENTATION_ITEM ( '' )  );
#28130=PRODUCT_DEFINITION_FORMATION_WITH_SPECIFIED_SOURCE ( 'ANY', '', #162165, .NOT_KNOWN. ) ;
#28276=EDGE_CURVE ( 'NONE', #151298, #43053, #120729, .T. ) ;
#28321=CARTESIAN_POINT ( 'NONE',  ( -16.81931177881023132, 9.936996059515063706, -154.7732178786172597 ) ) ;
#28368=CARTESIAN_POINT ( 'NONE',  ( -16.87036670365549895, 9.989418819312803066, -146.5204398826979855 ) ) ;
#28382=CARTESIAN_POINT ( 'NONE',  ( -16.94062896051973865, 9.992719105111833144, -146.6025165421188206 ) ) ;
#28532=DIRECTION ( 'NONE',  ( -0.000000000000000000, -0.000000000000000000, -1.000000000000000000 ) ) ;
#28592=CARTESIAN_POINT ( 'NONE',  ( -16.95709691156899268, 9.950000000011138823, -154.8399424374866271 ) ) ;
#28633=CARTESIAN_POINT ( 'NONE',  ( -18.37160782347004329, 11.47561641481354044, -143.2500000000000284 ) ) ;
#28721=CARTESIAN_POINT ( 'NONE',  ( -18.40000000000000213, 11.47316190337362762, -146.5500000000000114 ) ) ;
#28757=PLANE ( 'NONE',  #73538 ) ;
#28857=PLANE ( 'NONE',  #21553 ) ;
#28889=CYLINDRICAL_SURFACE ( 'NONE', #77446, 1.749999999999998002 ) ;
#29054=PLANE ( 'NONE',  #177410 ) ;
#29180=VECTOR ( 'NONE', #239129, 1000.000000000000000 ) ;
#29348=EDGE_CURVE ( 'NONE', #220835, #43053, #163629, .T. ) ;
#29520=CARTESIAN_POINT ( 'NONE',  ( -16.87036670365549895, 10.08494996326643189, -146.5500000000000114 ) ) ;
#29556=DIRECTION ( 'NONE',  ( 1.000000000000000000, 0.000000000000000000, -0.000000000000000000 ) ) ;
#29709=CARTESIAN_POINT ( 'NONE',  ( 13.99999999999999822, 9.850000000011137402, -150.7500000000000284 ) ) ;
#29890=CARTESIAN_POINT ( 'NONE',  ( -18.40000000000000213, 11.48667500176882328, -143.2500000000000284 ) ) ;
#29998=ORIENTED_EDGE ( 'NONE', *, *, #54344, .T. ) ;
#30470=DIRECTION ( 'NONE',  ( -1.000000000000000000, 0.000000000000000000, 0.000000000000000000 ) ) ;
#30604=DIRECTION ( 'NONE',  ( 0.000000000000000000, -0.000000000000000000, -1.000000000000000000 ) ) ;
#30692=DIRECTION ( 'NONE',  ( -1.000000000000000000, 0.000000000000000000, 0.000000000000000000 ) ) ;
#30899=ORIENTED_EDGE ( 'NONE', *, *, #53608, .F. ) ;
#31108=( BOUNDED_CURVE ( )  B_SPLINE_CURVE ( 3, ( #176525, #53988, #253461, #35741 ),
 .UNSPECIFIED., .F., .F. ) 
 B_SPLINE_CURVE_WITH_KNOTS ( ( 4, 4 ),
 ( 0.5235987755983901870, 1.570796326794896558 ),
 .UNSPECIFIED. ) 
 CURVE ( )  GEOMETRIC_REPRESENTATION_ITEM ( )  RATIONAL_B_SPLINE_CURVE ( ( 1.000000000000000000, 0.9106836025229743115, 0.9106836025229743115, 1.000000000000000000 ) ) 
 REPRESENTATION_ITEM ( '' )  );
#31125=CARTESIAN_POINT ( 'NONE',  ( -16.92989507731676113, 9.950000000011138823, -154.6174989306102248 ) ) ;
#31324=CARTESIAN_POINT ( 'NONE',  ( 20.27550659511089037, 9.216043722520002035, -146.6500000000000341 ) ) ;
#31495=CARTESIAN_POINT ( 'NONE',  ( -16.90128866880175806, 9.953795777214113016, -154.8626761833886576 ) ) ;
#31525=COLOUR_RGB ( '', 0.31764706, 0.68627451, 0.89019608) ;
#31535=VERTEX_POINT ( 'NONE', #45539 ) ;
#31536=AXIS2_PLACEMENT_3D ( 'NONE', #84966, #8047, #164552 ) ;
#31627=CARTESIAN_POINT ( 'NONE',  ( 12.25000000000000000, 9.350000000011140955, -150.7500000000000284 ) ) ;
#31712=CARTESIAN_POINT ( 'NONE',  ( -16.89268316805465986, 9.951721813253337601, -154.8557524785455541 ) ) ;
#32215=CARTESIAN_POINT ( 'NONE',  ( -16.93230518875208546, 10.00075036143099894, -146.5757783481015508 ) ) ;
#32325=CARTESIAN_POINT ( 'NONE',  ( -14.77738660682463667, 9.436552840015577814, -149.1779554727603454 ) ) ;
#32401=CARTESIAN_POINT ( 'NONE',  ( -16.81744102076748959, 9.950000000011138823, -154.8500000000000227 ) ) ;
#32774=AXIS2_PLACEMENT_3D ( 'NONE', #214850, #16675, #96173 ) ;
#32877=CARTESIAN_POINT ( 'NONE',  ( -16.93234230245721861, 9.998107370558241058, -154.9176902816662675 ) ) ;
#33228=FACE_OUTER_BOUND ( 'NONE', #9073, .T. ) ;
#33720=AXIS2_PLACEMENT_3D ( 'NONE', #249157, #190478, #189168 ) ;
#33885=EDGE_LOOP ( 'NONE', ( #190313, #80038, #7615, #186101 ) ) ;
#33928=AXIS2_PLACEMENT_3D ( 'NONE', #247572, #149783, #230591 ) ;
#34046=LINE ( 'NONE', #251769, #108135 ) ;
#34124=CARTESIAN_POINT ( 'NONE',  ( -18.36973785203556275, 11.47550320049537476, -158.2500000000000284 ) ) ;
#34156=CARTESIAN_POINT ( 'NONE',  ( -16.93353400591625757, 10.00461239618409515, -154.9326844702054586 ) ) ;
#34332=CARTESIAN_POINT ( 'NONE',  ( -16.92507428761701860, 9.950000000011138823, -154.7866025403784249 ) ) ;
#34567=DIRECTION ( 'NONE',  ( -1.020425574104004196E-15, -0.000000000000000000, -1.000000000000000000 ) ) ;
#34648=CARTESIAN_POINT ( 'NONE',  ( -16.93388492042257809, 9.988541822527057690, -154.9005451231862196 ) ) ;
#35343=CARTESIAN_POINT ( 'NONE',  ( -16.90202395485792408, 9.965944544561779139, -146.5969862787401325 ) ) ;
#35437=VECTOR ( 'NONE', #54811, 1000.000000000000000 ) ;
#35478=EDGE_CURVE ( 'NONE', #88823, #254838, #124947, .T. ) ;
#35525=DIRECTION ( 'NONE',  ( -0.000000000000000000, -0.000000000000000000, -1.000000000000000000 ) ) ;
#35663=DIRECTION ( 'NONE',  ( -1.000000000000000000, -0.000000000000000000, -0.000000000000000000 ) ) ;
#35739=ORIENTED_EDGE ( 'NONE', *, *, #84262, .F. ) ;
#35741=CARTESIAN_POINT ( 'NONE',  ( -17.11825945287482753, 9.950000000011138823, -146.7500000000000284 ) ) ;
#35774=DIRECTION ( 'NONE',  ( -0.000000000000000000, -0.000000000000000000, -1.000000000000000000 ) ) ;
#36162=CARTESIAN_POINT ( 'NONE',  ( -12.24999999999999822, 9.350000000011132073, -150.5185689574026355 ) ) ;
#36190=CARTESIAN_POINT ( 'NONE',  ( -16.77683809663752257, 9.950000000011138823, -154.8500000000000227 ) ) ;
#36721=DIRECTION ( 'NONE',  ( -1.073024830501117725E-15, 0.000000000000000000, 1.000000000000000000 ) ) ;
#36869=ORIENTED_EDGE ( 'NONE', *, *, #214868, .T. ) ;
#36960=AXIS2_PLACEMENT_3D ( 'NONE', #3118, #241746, #80066 ) ;
#37012=EDGE_LOOP ( 'NONE', ( #167976, #39300, #21523, #102465 ) ) ;
#37107=CARTESIAN_POINT ( 'NONE',  ( -16.87683809663752399, 9.865889849343238538, -154.2325731929306016 ) ) ;
#37356=VECTOR ( 'NONE', #132717, 1000.000000000000000 ) ;
#37360=AXIS2_PLACEMENT_3D ( 'NONE', #87899, #102314, #24128 ) ;
#37454=ORIENTED_EDGE ( 'NONE', *, *, #70285, .T. ) ;
#37558=CARTESIAN_POINT ( 'NONE',  ( -16.97683809663752186, 9.950000000011138823, -143.2500000000000284 ) ) ;
#37858=CARTESIAN_POINT ( 'NONE',  ( 23.24999999999999645, 11.75000000001113953, -154.8500000000000227 ) ) ;
#37865=EDGE_CURVE ( 'NONE', #221, #168716, #249, .T. ) ;
#37922=AXIS2_PLACEMENT_3D ( 'NONE', #18244, #235993, #131764 ) ;
#38218=DIRECTION ( 'NONE',  ( 0.000000000000000000, 0.000000000000000000, 1.000000000000000000 ) ) ;
#38343=( BOUNDED_CURVE ( )  B_SPLINE_CURVE ( 3, ( #138760, #176666, #203592, #557 ),
 .UNSPECIFIED., .F., .T. ) 
 B_SPLINE_CURVE_WITH_KNOTS ( ( 4, 4 ),
 ( 2.589852378279005940, 2.850972632318390598 ),
 .UNSPECIFIED. ) 
 CURVE ( )  GEOMETRIC_REPRESENTATION_ITEM ( )  RATIONAL_B_SPLINE_CURVE ( ( 1.000000000000000000, 0.9943260843901261525, 0.9943260843901261525, 1.000000000000000000 ) ) 
 REPRESENTATION_ITEM ( '' )  );
#38469=DIRECTION ( 'NONE',  ( -0.000000000000000000, 1.000000000000000000, -0.000000000000000000 ) ) ;
#38717=CARTESIAN_POINT ( 'NONE',  ( -12.25000000000000178, 9.350000000011139178, -150.7500000000000284 ) ) ;
#38740=EDGE_CURVE ( 'NONE', #11705, #168403, #21457, .T. ) ;
#38847=CARTESIAN_POINT ( 'NONE',  ( 22.88900146558018989, 8.703904791123973084, -146.6500000000000341 ) ) ;
#38857=CYLINDRICAL_SURFACE ( 'NONE', #195665, 1.749999999999999778 ) ;
#39025=VERTEX_POINT ( 'NONE', #231214 ) ;
#39130=CARTESIAN_POINT ( 'NONE',  ( -16.87036670365549895, 9.989418819312803066, -146.5204398826979855 ) ) ;
#39257=CIRCLE ( 'NONE', #126717, 0.5000000000000004441 ) ;
#39265=DIRECTION ( 'NONE',  ( -0.000000000000000000, -0.000000000000000000, -1.000000000000000000 ) ) ;
#39300=ORIENTED_EDGE ( 'NONE', *, *, #236138, .F. ) ;
#39411=DIRECTION ( 'NONE',  ( -1.000000000000000000, 0.000000000000000000, 0.000000000000000000 ) ) ;
#39455=EDGE_CURVE ( 'NONE', #138980, #49221, #63491, .T. ) ;
#39858=AXIS2_PLACEMENT_3D ( 'NONE', #249893, #150791, #71278 ) ;
#39863=VECTOR ( 'NONE', #238730, 1000.000000000000000 ) ;
#39922=CYLINDRICAL_SURFACE ( 'NONE', #1696, 1.500000000000001332 ) ;
#40118=DIRECTION ( 'NONE',  ( -0.000000000000000000, 1.000000000000000000, -0.000000000000000000 ) ) ;
#40347=ORIENTED_EDGE ( 'NONE', *, *, #153047, .F. ) ;
#40682=DIRECTION ( 'NONE',  ( 1.000000000000000000, 0.000000000000000000, 0.000000000000000000 ) ) ;
#40706=LINE ( 'NONE', #2801, #13183 ) ;
#40868=VECTOR ( 'NONE', #14835, 1000.000000000000000 ) ;
#41032=FACE_OUTER_BOUND ( 'NONE', #60795, .T. ) ;
#41200=FACE_OUTER_BOUND ( 'NONE', #123876, .T. ) ;
#41457=EDGE_CURVE ( 'NONE', #221934, #5552, #212338, .T. ) ;
#41627=CARTESIAN_POINT ( 'NONE',  ( 16.27683809663749770, 9.350000000011137402, -143.2500000000000284 ) ) ;
#41958=CARTESIAN_POINT ( 'NONE',  ( 15.75000000000000000, 9.350000000011142731, -150.5185689574027208 ) ) ;
#41968=DIRECTION ( 'NONE',  ( -1.073024830501117725E-15, -0.000000000000000000, -1.000000000000000000 ) ) ;
#42064=CARTESIAN_POINT ( 'NONE',  ( -16.88783316861821859, 9.950000000011137047, -146.7522640419797995 ) ) ;
#42485=FILL_AREA_STYLE_COLOUR ( '', #31525 ) ;
#42756=DIRECTION ( 'NONE',  ( 1.000000000000000000, 1.186688945009009831E-16, 0.000000000000000000 ) ) ;
#43053=VERTEX_POINT ( 'NONE', #135223 ) ;
#43125=ORIENTED_EDGE ( 'NONE', *, *, #66648, .F. ) ;
#43225=CARTESIAN_POINT ( 'NONE',  ( 14.77516762759920788, 9.436674251854004325, -149.1768619309991948 ) ) ;
#43321=ORIENTED_EDGE ( 'NONE', *, *, #211440, .T. ) ;
#43443=DIRECTION ( 'NONE',  ( -0.5932847527679299127, 0.8049926720990051576, 6.366092712777055223E-16 ) ) ;
#43558=VERTEX_POINT ( 'NONE', #158385 ) ;
#43642=CARTESIAN_POINT ( 'NONE',  ( -21.65000000000000213, 9.950000000011138823, -146.7500000000000284 ) ) ;
#43660=CARTESIAN_POINT ( 'NONE',  ( -16.81930730667006912, 9.936998068885202429, -146.7267677305382279 ) ) ;
#43663=DIRECTION ( 'NONE',  ( 1.020425574104004196E-15, 1.210927747993693964E-31, -1.000000000000000000 ) ) ;
#43781=( NAMED_UNIT ( * ) SI_UNIT ( $, .STERADIAN. ) SOLID_ANGLE_UNIT ( ) );
#43832=CARTESIAN_POINT ( 'NONE',  ( 12.42718393586866910, 9.370655051134638924, -151.5258232559808960 ) ) ;
#43878=ADVANCED_FACE ( 'NONE', ( #138449 ), #242127, .T. ) ;
#43967=ORIENTED_EDGE ( 'NONE', *, *, #77049, .F. ) ;
#43975=B_SPLINE_CURVE_WITH_KNOTS ( 'NONE', 3,
 ( #212145, #162447, #59431, #118166 ),
 .UNSPECIFIED., .F., .F.,
 ( 4, 4 ),
 ( 0.000000000000000000, 7.713889350930393175E-05 ),
 .UNSPECIFIED. ) ;
#43985=VERTEX_POINT ( 'NONE', #221838 ) ;
#43991=CARTESIAN_POINT ( 'NONE',  ( -16.87683809663752399, 9.850000000011144508, -154.0976359818037054 ) ) ;
#44395=EDGE_CURVE ( 'NONE', #206656, #115602, #106398, .T. ) ;
#44403=DIRECTION ( 'NONE',  ( 1.186688945009010077E-16, -1.000000000000000000, -0.000000000000000000 ) ) ;
#44515=CARTESIAN_POINT ( 'NONE',  ( 13.12220780326572189, 9.430633469083952392, -149.2317657948241276 ) ) ;
#44620=CARTESIAN_POINT ( 'NONE',  ( -16.87401514999234919, 9.950000000011137047, -146.7199820074679337 ) ) ;
#44915=CARTESIAN_POINT ( 'NONE',  ( -15.69373346032659100, 9.356790025057035720, -151.2048265086139054 ) ) ;
#44949=CARTESIAN_POINT ( 'NONE',  ( 18.39999999999999503, 5.650000000011139001, -146.6500000000000341 ) ) ;
#44983=ORIENTED_EDGE ( 'NONE', *, *, #110894, .F. ) ;
#44985=CARTESIAN_POINT ( 'NONE',  ( 18.39999999999999503, 5.650000000011139001, -146.6500000000000341 ) ) ;
#45118=CARTESIAN_POINT ( 'NONE',  ( 18.39999999999997371, 11.47316190337362940, -158.2500000000000284 ) ) ;
#45539=CARTESIAN_POINT ( 'NONE',  ( -15.75000000000000355, 9.350000000011140955, -150.7500000000000284 ) ) ;
#45629=VECTOR ( 'NONE', #7557, 1000.000000000000000 ) ;
#45717=VERTEX_POINT ( 'NONE', #76266 ) ;
#45895=CARTESIAN_POINT ( 'NONE',  ( -16.93710578446423654, 9.950000000011137047, -146.9188039837998758 ) ) ;
#46057=VECTOR ( 'NONE', #126704, 1000.000000000000000 ) ;
#46324=EDGE_CURVE ( 'NONE', #83264, #209017, #200595, .T. ) ;
#46541=CARTESIAN_POINT ( 'NONE',  ( -16.83199318825829494, 9.930646127992320160, -154.7275851882092184 ) ) ;
#46804=ORIENTED_EDGE ( 'NONE', *, *, #72263, .T. ) ;
#47049=CARTESIAN_POINT ( 'NONE',  ( 14.56326696814970489, 9.446648990640015953, -149.0891632959232140 ) ) ;
#47139=CARTESIAN_POINT ( 'NONE',  ( -20.65000000000000568, 7.250000000011138646, -154.8500000000000227 ) ) ;
#47153=CARTESIAN_POINT ( 'NONE',  ( -16.82055514392377304, 9.950000000011137047, -146.6767980745422619 ) ) ;
#47365=ORIENTED_EDGE ( 'NONE', *, *, #215198, .F. ) ;
#47511=ORIENTED_EDGE ( 'NONE', *, *, #4342, .T. ) ;
#47656=ORIENTED_EDGE ( 'NONE', *, *, #11738, .F. ) ;
#47666=CARTESIAN_POINT ( 'NONE',  ( -18.34374000495059676, 11.47316190337362940, -158.2500000000000284 ) ) ;
#48002=DIRECTION ( 'NONE',  ( 0.000000000000000000, 0.000000000000000000, 1.000000000000000000 ) ) ;
#48233=ORIENTED_EDGE ( 'NONE', *, *, #196813, .F. ) ;
#48265=FACE_OUTER_BOUND ( 'NONE', #116256, .T. ) ;
#48283=DIRECTION ( 'NONE',  ( 0.000000000000000000, 0.000000000000000000, 1.000000000000000000 ) ) ;
#48567=ORIENTED_EDGE ( 'NONE', *, *, #155194, .F. ) ;
#48722=CYLINDRICAL_SURFACE ( 'NONE', #64366, 0.9000000000000014655 ) ;
#48791=FACE_OUTER_BOUND ( 'NONE', #90178, .T. ) ;
#49118=VERTEX_POINT ( 'NONE', #7317 ) ;
#49221=VERTEX_POINT ( 'NONE', #90379 ) ;
#49262=EDGE_CURVE ( 'NONE', #49118, #121114, #209056, .T. ) ;
#49533=ORIENTED_EDGE ( 'NONE', *, *, #89401, .T. ) ;
#49564=AXIS2_PLACEMENT_3D ( 'NONE', #153211, #136145, #30692 ) ;
#49738=CARTESIAN_POINT ( 'NONE',  ( -16.91776028072577631, 9.963400393640901243, -154.8750240147021486 ) ) ;
#49783=FACE_OUTER_BOUND ( 'NONE', #72412, .T. ) ;
#50199=CARTESIAN_POINT ( 'NONE',  ( 21.13736287352038445, 8.046642376395153562, -143.2500000000000284 ) ) ;
#50326=CARTESIAN_POINT ( 'NONE',  ( -18.40000000000000213, 11.47316190337364183, -158.1740539331920559 ) ) ;
#50358=ORIENTED_EDGE ( 'NONE', *, *, #152381, .T. ) ;
#50766=ORIENTED_EDGE ( 'NONE', *, *, #11224, .F. ) ;
#50904=CARTESIAN_POINT ( 'NONE',  ( -16.87036670365549895, 9.989418819312803066, -146.5204398826979855 ) ) ;
#51246=CYLINDRICAL_SURFACE ( 'NONE', #15723, 0.1000000000000001443 ) ;
#51381=CARTESIAN_POINT ( 'NONE',  ( 23.24999999999999645, 11.75000000001113953, -143.2500000000000284 ) ) ;
#51429=DIRECTION ( 'NONE',  ( -1.652117596168391700E-15, -1.000000000000000000, 0.000000000000000000 ) ) ;
#51656=CARTESIAN_POINT ( 'NONE',  ( 21.72449340488910252, 10.28395627750227526, -143.2500000000000284 ) ) ;
#51667=( BOUNDED_CURVE ( )  B_SPLINE_CURVE ( 3, ( #50326, #226394, #92038, #148162 ),
 .UNSPECIFIED., .F., .T. ) 
 B_SPLINE_CURVE_WITH_KNOTS ( ( 4, 4 ),
 ( 5.733388419619902088, 5.983100554402347449 ),
 .UNSPECIFIED. ) 
 CURVE ( )  GEOMETRIC_REPRESENTATION_ITEM ( )  RATIONAL_B_SPLINE_CURVE ( ( 1.000000000000000000, 0.9948104011409417691, 0.9948104011409417691, 1.000000000000000000 ) ) 
 REPRESENTATION_ITEM ( '' )  );
#51724=CARTESIAN_POINT ( 'NONE',  ( -16.93262454970420094, 10.00202046794151300, -146.5729237737627102 ) ) ;
#51832=CARTESIAN_POINT ( 'NONE',  ( -14.11697426661281440, 9.457410944778567696, -149.0000839737900549 ) ) ;
#52098=DIRECTION ( 'NONE',  ( -1.000000000000000000, 0.000000000000000000, 0.000000000000000000 ) ) ;
#52192=CARTESIAN_POINT ( 'NONE',  ( -20.65000000000000568, 7.250000000011138646, -146.6500000000000341 ) ) ;
#52276=CARTESIAN_POINT ( 'NONE',  ( -16.92973740335376220, 9.992503814478528312, -146.5939409647978664 ) ) ;
#52312=( GEOMETRIC_REPRESENTATION_CONTEXT ( 3 ) GLOBAL_UNCERTAINTY_ASSIGNED_CONTEXT ( ( #13821 ) ) GLOBAL_UNIT_ASSIGNED_CONTEXT ( ( #120776, #81583, #63325 ) ) REPRESENTATION_CONTEXT ( 'NONE', 'WORKASPACE' ) );
#52319=ORIENTED_EDGE ( 'NONE', *, *, #135002, .F. ) ;
#52570=FACE_OUTER_BOUND ( 'NONE', #33885, .T. ) ;
#52925=CARTESIAN_POINT ( 'NONE',  ( -16.87683809663752399, 9.850000000011123191, -147.4023640181965220 ) ) ;
#52996=ORIENTED_EDGE ( 'NONE', *, *, #29348, .T. ) ;
#53118=VECTOR ( 'NONE', #43663, 1000.000000000000000 ) ;
#53425=CARTESIAN_POINT ( 'NONE',  ( -16.77683809663752257, 9.945835743215303282, -154.8360509808958057 ) ) ;
#53540=CARTESIAN_POINT ( 'NONE',  ( -18.39999999999999858, 11.75000000001113953, -143.2500000000000284 ) ) ;
#53586=CARTESIAN_POINT ( 'NONE',  ( -16.92570016628984320, 9.958788957751020021, -146.6206506700390264 ) ) ;
#53608=EDGE_CURVE ( 'NONE', #127092, #139553, #239788, .T. ) ;
#53617=EDGE_CURVE ( 'NONE', #67383, #129669, #14662, .T. ) ;
#53663=ORIENTED_EDGE ( 'NONE', *, *, #55725, .T. ) ;
#53756=AXIS2_PLACEMENT_3D ( 'NONE', #7519, #205710, #162764 ) ;
#53810=CARTESIAN_POINT ( 'NONE',  ( -16.88460203013676875, 9.954759003246872240, -154.8658918095382546 ) ) ;
#53988=CARTESIAN_POINT ( 'NONE',  ( -16.92507428761702926, 9.950000000011137047, -146.7133974596215751 ) ) ;
#53994=EDGE_CURVE ( 'NONE', #39025, #168716, #167692, .T. ) ;
#54066=CARTESIAN_POINT ( 'NONE',  ( -16.87401514999227814, 9.950000000011137047, -154.7800179925321231 ) ) ;
#54134=EDGE_CURVE ( 'NONE', #71322, #212672, #212442, .T. ) ;
#54307=CARTESIAN_POINT ( 'NONE',  ( -16.93302609847409457, 9.996682520814371031, -146.5863884953625700 ) ) ;
#54314=VECTOR ( 'NONE', #143615, 1000.000000000000000 ) ;
#54344=EDGE_CURVE ( 'NONE', #190690, #159239, #214447, .T. ) ;
#54419=CARTESIAN_POINT ( 'NONE',  ( -12.25000000000000178, 9.350000000011139178, -150.7500000000000284 ) ) ;
#54657=ORIENTED_EDGE ( 'NONE', *, *, #181583, .T. ) ;
#54811=DIRECTION ( 'NONE',  ( 0.000000000000000000, -1.000000000000000000, 0.000000000000000000 ) ) ;
#54845=CARTESIAN_POINT ( 'NONE',  ( -16.85718274719486587, 9.976142314632873820, -146.5633463321825616 ) ) ;
#54871=EDGE_CURVE ( 'NONE', #141855, #9223, #84873, .T. ) ;
#55215=VERTEX_POINT ( 'NONE', #52192 ) ;
#55655=CARTESIAN_POINT ( 'NONE',  ( 20.99999999999999645, 9.750000000011137757, -154.8500000000000227 ) ) ;
#55725=EDGE_CURVE ( 'NONE', #157401, #212672, #68280, .T. ) ;
#55975=VECTOR ( 'NONE', #248072, 1000.000000000000000 ) ;
#56149=ORIENTED_EDGE ( 'NONE', *, *, #243074, .T. ) ;
#56249=VERTEX_POINT ( 'NONE', #53540 ) ;
#56388=ORIENTED_EDGE ( 'NONE', *, *, #243120, .F. ) ;
#56530=LINE ( 'NONE', #215623, #250207 ) ;
#56540=VERTEX_POINT ( 'NONE', #143472 ) ;
#56610=ORIENTED_EDGE ( 'NONE', *, *, #63862, .T. ) ;
#57192=CARTESIAN_POINT ( 'NONE',  ( -18.34374000495060386, 11.47316190337362585, -143.2500000000000284 ) ) ;
#57512=CARTESIAN_POINT ( 'NONE',  ( -16.94132844910802760, 9.992436755191501874, -154.8962017559823323 ) ) ;
#57595=ADVANCED_FACE ( 'NONE', ( #33228 ), #189694, .F. ) ;
#57645=EDGE_LOOP ( 'NONE', ( #43125, #256949, #132557 ) ) ;
#57697=CARTESIAN_POINT ( 'NONE',  ( -17.01473183483381391, 9.950000000011138823, -154.7500000000000284 ) ) ;
#57827=ORIENTED_EDGE ( 'NONE', *, *, #243074, .F. ) ;
#57904=CARTESIAN_POINT ( 'NONE',  ( -16.83233564386398839, 9.930221796595855466, -154.7245206634761132 ) ) ;
#57922=ORIENTED_EDGE ( 'NONE', *, *, #44395, .F. ) ;
#57951=VECTOR ( 'NONE', #14164, 1000.000000000000000 ) ;
#58295=CARTESIAN_POINT ( 'NONE',  ( -16.78055652883087134, 9.946776916136505164, -146.6607918375924555 ) ) ;
#58383=ORIENTED_EDGE ( 'NONE', *, *, #250428, .F. ) ;
#58755=B_SPLINE_CURVE_WITH_KNOTS ( 'NONE', 3,
 ( #254900, #78870, #253663, #237958, #59286, #155896, #138826, #154614, #235391, #218385, #3188, #141433, #5754, #181855, #202691, #162304, #4482, #241819, #64481, #20219, #24086, #119313, #198838, #63171, #200135, #100974, #44915, #201404, #103569, #140133 ),
 .UNSPECIFIED., .F., .F.,
 ( 4, 2, 2, 2, 2, 2, 2, 2, 2, 2, 2, 2, 2, 2, 4 ),
 ( 0.000000000000000000, 0.0003422764154113111176, 0.0006845528308226222353, 0.001026829246233933353, 0.001369105661645244471, 0.002053658492467925253, 0.002738211323290606469, 0.003080487738701950112, 0.003422764154113292889, 0.003765040569524635665, 0.004107316984935978008, 0.004449593400347320350, 0.004791869815758663560, 0.005134146231170005903, 0.005476422646581349113 ),
 .UNSPECIFIED. ) ;
#58927=EDGE_LOOP ( 'NONE', ( #147936, #241178, #47656, #50358 ) ) ;
#58997=CARTESIAN_POINT ( 'NONE',  ( -16.86132326855786090, 9.950000000011137047, -146.6986357846683688 ) ) ;
#59083=ORIENTED_EDGE ( 'NONE', *, *, #158042, .F. ) ;
#59286=CARTESIAN_POINT ( 'NONE',  ( -12.33960340485503870, 9.360749169926261715, -151.3145701406073158 ) ) ;
#59289=VERTEX_POINT ( 'NONE', #137160 ) ;
#59431=CARTESIAN_POINT ( 'NONE',  ( -18.40000000000000213, 11.47316190337310537, -158.2001707515343014 ) ) ;
#59466=CARTESIAN_POINT ( 'NONE',  ( -16.87036670365548474, 10.08494996326643189, -154.9500000000000455 ) ) ;
#59831=CIRCLE ( 'NONE', #118111, 0.09999999999998898659 ) ;
#59924=CARTESIAN_POINT ( 'NONE',  ( -14.00000000000000178, 9.850000000011133849, -150.7500000000000284 ) ) ;
#60020=DIRECTION ( 'NONE',  ( -0.000000000000000000, 1.000000000000000000, -0.000000000000000000 ) ) ;
#60054=ADVANCED_FACE ( 'NONE', ( #167545 ), #22897, .F. ) ;
#60777=DIRECTION ( 'NONE',  ( 0.000000000000000000, -0.9553114395363172529, -0.2956011730204217702 ) ) ;
#60795=EDGE_LOOP ( 'NONE', ( #115103, #109166, #190071, #138093 ) ) ;
#60839=ORIENTED_EDGE ( 'NONE', *, *, #103498, .F. ) ;
#60840=EDGE_LOOP ( 'NONE', ( #239616, #9174, #196807, #47511, #85051, #103626 ) ) ;
#61140=CARTESIAN_POINT ( 'NONE',  ( -23.25000000000000355, 5.650000000011139001, -146.6500000000000341 ) ) ;
#61163=ORIENTED_EDGE ( 'NONE', *, *, #155194, .T. ) ;
#61237=CARTESIAN_POINT ( 'NONE',  ( -16.89268316805466341, 9.951721813253341153, -146.6442475214544743 ) ) ;
#61353=AXIS2_PLACEMENT_3D ( 'NONE', #96451, #191760, #176040 ) ;
#61494=EDGE_CURVE ( 'NONE', #217779, #7029, #74143, .T. ) ;
#61598=DIRECTION ( 'NONE',  ( 0.000000000000000000, 0.000000000000000000, -1.000000000000000000 ) ) ;
#61940=LINE ( 'NONE', #144026, #53118 ) ;
#61968=ORIENTED_EDGE ( 'NONE', *, *, #129940, .F. ) ;
#62048=ORIENTED_EDGE ( 'NONE', *, *, #184140, .T. ) ;
#62114=CARTESIAN_POINT ( 'NONE',  ( 12.93279065517211635, 9.417690691074255938, -152.1416006967646695 ) ) ;
#62456=VERTEX_POINT ( 'NONE', #158216 ) ;
#62487=ORIENTED_EDGE ( 'NONE', *, *, #130674, .T. ) ;
#62785=CARTESIAN_POINT ( 'NONE',  ( 15.70340296795548163, 9.355888454513701546, -150.2886428967780148 ) ) ;
#63002=ORIENTED_EDGE ( 'NONE', *, *, #148686, .F. ) ;
#63171=CARTESIAN_POINT ( 'NONE',  ( -15.51798037960204191, 9.376659938544687378, -151.6281925482172710 ) ) ;
#63222=VECTOR ( 'NONE', #101511, 1000.000000000000000 ) ;
#63320=DIRECTION ( 'NONE',  ( 0.000000000000000000, 0.000000000000000000, -1.000000000000000000 ) ) ;
#63322=CARTESIAN_POINT ( 'NONE',  ( -16.87487986503753845, 9.950007555096753720, -146.6499747396867406 ) ) ;
#63325=( NAMED_UNIT ( * ) SI_UNIT ( $, .STERADIAN. ) SOLID_ANGLE_UNIT ( ) );
#63328=ORIENTED_EDGE ( 'NONE', *, *, #162397, .F. ) ;
#63402=VECTOR ( 'NONE', #114939, 1000.000000000000000 ) ;
#63487=SHAPE_REPRESENTATION ( 'Snap Open Cable Crossbars 5', ( #2425 ), #227291 ) ;
#63491=B_SPLINE_CURVE_WITH_KNOTS ( 'NONE', 3,
 ( #39130, #159082, #118667, #82045, #196888, #221567, #198175, #18261, #1241, #61237 ),
 .UNSPECIFIED., .F., .F.,
 ( 4, 3, 3, 4 ),
 ( 0.000000000000000000, 4.874959354401679605E-05, 9.785140065121436244E-05, 0.0001360444631935818385 ),
 .UNSPECIFIED. ) ;
#63776=CARTESIAN_POINT ( 'NONE',  ( -21.65000000000000213, 9.950000000011140600, -154.7500000000000284 ) ) ;
#63862=EDGE_CURVE ( 'NONE', #93783, #242248, #39257, .T. ) ;
#64136=DIRECTION ( 'NONE',  ( -0.7071067811865562325, -0.7071067811865388020, 0.000000000000000000 ) ) ;
#64366=AXIS2_PLACEMENT_3D ( 'NONE', #70895, #128278, #112571 ) ;
#64372=ORIENTED_EDGE ( 'NONE', *, *, #85825, .F. ) ;
#64405=ADVANCED_FACE ( 'NONE', ( #180727 ), #142841, .F. ) ;
#64481=CARTESIAN_POINT ( 'NONE',  ( -14.87770893841224940, 9.430637101707896264, -152.2682606180609639 ) ) ;
#64875=CARTESIAN_POINT ( 'NONE',  ( -16.97683809663752186, 9.850000000011140955, -146.6500000000000341 ) ) ;
#64888=CARTESIAN_POINT ( 'NONE',  ( -16.93909480342659890, 9.993078364812696179, -146.6003470166723446 ) ) ;
#65133=CARTESIAN_POINT ( 'NONE',  ( -16.92778301347364689, 10.00094491684727771, -154.9285181079674487 ) ) ;
#65249=CARTESIAN_POINT ( 'NONE',  ( 23.04999999999999716, 8.822561741677553471, -154.8500000000000227 ) ) ;
#65329=PRESENTATION_STYLE_ASSIGNMENT (( #144859 ) ) ;
#65392=FACE_OUTER_BOUND ( 'NONE', #77992, .T. ) ;
#65451=CARTESIAN_POINT ( 'NONE',  ( -16.83233564386404169, 9.930221796595757766, -146.7754793365243984 ) ) ;
#65702=CIRCLE ( 'NONE', #219813, 1.500000000000001332 ) ;
#65753=ORIENTED_EDGE ( 'NONE', *, *, #11224, .T. ) ;
#65958=CARTESIAN_POINT ( 'NONE',  ( 15.74999999999999645, 9.350000000011139178, -150.7500000000000284 ) ) ;
#66086=UNCERTAINTY_MEASURE_WITH_UNIT (LENGTH_MEASURE( 1.000000000000000082E-05 ), #179460, 'distance_accuracy_value', 'NONE');
#66113=DIRECTION ( 'NONE',  ( -0.000000000000000000, 1.000000000000000000, -0.000000000000000000 ) ) ;
#66124=CARTESIAN_POINT ( 'NONE',  ( -16.79140778683508728, 9.944941598865716159, -154.8297372337707998 ) ) ;
#66167=DIRECTION ( 'NONE',  ( -1.000000000000000000, 0.000000000000000000, 0.000000000000000000 ) ) ;
#66208=CARTESIAN_POINT ( 'NONE',  ( -16.27683809663751191, 9.350000000011132073, -146.5500000000000114 ) ) ;
#66493=ADVANCED_FACE ( 'NONE', ( #213507 ), #227947, .F. ) ;
#66495=ORIENTED_EDGE ( 'NONE', *, *, #159188, .T. ) ;
#66523=CARTESIAN_POINT ( 'NONE',  ( -18.40000000000000213, 11.41458325961093756, -146.6500000000000057 ) ) ;
#66598=CARTESIAN_POINT ( 'NONE',  ( -16.92209698673723395, 9.950000000011138823, -146.7106355670536573 ) ) ;
#66637=CARTESIAN_POINT ( 'NONE',  ( 12.84233041328156588, 9.410538608540022665, -149.4326879971409596 ) ) ;
#66648=EDGE_CURVE ( 'NONE', #136679, #103596, #99956, .T. ) ;
#66837=ORIENTED_EDGE ( 'NONE', *, *, #158264, .T. ) ;
#66858=ORIENTED_EDGE ( 'NONE', *, *, #245669, .T. ) ;
#66917=CARTESIAN_POINT ( 'NONE',  ( -18.39999999999999858, 11.47867410001042998, -143.2746932163406655 ) ) ;
#66928=ORIENTED_EDGE ( 'NONE', *, *, #79968, .T. ) ;
#67353=CARTESIAN_POINT ( 'NONE',  ( -18.40000000000000213, 11.41458325961095177, -154.8500000000000512 ) ) ;
#67383=VERTEX_POINT ( 'NONE', #181492 ) ;
#67487=EDGE_LOOP ( 'NONE', ( #168816, #256565, #97287, #248470, #12525, #106314 ) ) ;
#68103=VECTOR ( 'NONE', #117790, 1000.000000000000000 ) ;
#68116=CARTESIAN_POINT ( 'NONE',  ( 18.54999999999999716, 8.750000000011182166, -146.6500000000000341 ) ) ;
#68179=ADVANCED_FACE ( 'NONE', ( #152718 ), #257299, .T. ) ;
#68280=LINE ( 'NONE', #69573, #243396 ) ;
#68466=CARTESIAN_POINT ( 'NONE',  ( 23.24999999999999645, 5.650000000011139001, -146.6500000000000341 ) ) ;
#68724=ADVANCED_FACE ( 'NONE', ( #177098 ), #38857, .F. ) ;
#68781=ORIENTED_EDGE ( 'NONE', *, *, #101129, .F. ) ;
#68856=VECTOR ( 'NONE', #93186, 1000.000000000000000 ) ;
#68880=FACE_OUTER_BOUND ( 'NONE', #226400, .T. ) ;
#69032=DIRECTION ( 'NONE',  ( 1.000000000000000000, 1.186688945009010077E-16, 0.000000000000000000 ) ) ;
#69039=DIRECTION ( 'NONE',  ( 0.000000000000000000, 0.000000000000000000, -1.000000000000000000 ) ) ;
#69152=ORIENTED_EDGE ( 'NONE', *, *, #181583, .F. ) ;
#69321=CARTESIAN_POINT ( 'NONE',  ( -16.94275863006528482, 9.989496048678669027, -154.8916973820765861 ) ) ;
#69363=CARTESIAN_POINT ( 'NONE',  ( -16.87331047859649757, 9.950000000011138823, -154.8500000000000227 ) ) ;
#69573=CARTESIAN_POINT ( 'NONE',  ( 18.39999999999999503, 11.47316190337363828, -158.2500000000000284 ) ) ;
#69574=DIRECTION ( 'NONE',  ( 0.7071067811865463515, -0.7071067811865487940, 0.000000000000000000 ) ) ;
#70072=VERTEX_POINT ( 'NONE', #242208 ) ;
#70116=PLANE ( 'NONE',  #236693 ) ;
#70285=EDGE_CURVE ( 'NONE', #43985, #203363, #693, .T. ) ;
#70321=EDGE_CURVE ( 'NONE', #43558, #225791, #180653, .T. ) ;
#70358=ORIENTED_EDGE ( 'NONE', *, *, #215198, .T. ) ;
#70437=CARTESIAN_POINT ( 'NONE',  ( -18.40000000000000213, 5.650000000011139001, -146.6500000000000341 ) ) ;
#70465=CARTESIAN_POINT ( 'NONE',  ( 20.73486653747088937, 7.750000000011182166, -143.2500000000000284 ) ) ;
#70622=CARTESIAN_POINT ( 'NONE',  ( -16.94052228080551359, 9.986279733109993728, -154.8903755026694569 ) ) ;
#70844=PRODUCT_DEFINITION ( 'UNKNOWN', '', #28130, #154952 ) ;
#70895=CARTESIAN_POINT ( 'NONE',  ( 20.99999999999999645, 9.750000000011137757, -143.2500000000000284 ) ) ;
#70954=LINE ( 'NONE', #150472, #190472 ) ;
#71051=CARTESIAN_POINT ( 'NONE',  ( -21.64999999999999858, 9.350000000011133849, -143.2500000000000284 ) ) ;
#71199=DIRECTION ( 'NONE',  ( 0.000000000000000000, 0.9553114395363172529, -0.2956011730204217702 ) ) ;
#71278=DIRECTION ( 'NONE',  ( -1.000000000000000000, 3.854941057726231589E-15, 0.000000000000000000 ) ) ;
#71313=VERTEX_POINT ( 'NONE', #111705 ) ;
#71322=VERTEX_POINT ( 'NONE', #118123 ) ;
#71324=EDGE_LOOP ( 'NONE', ( #95732, #154813, #207958, #150374, #139594 ) ) ;
#71442=CARTESIAN_POINT ( 'NONE',  ( -14.23072895065543086, 9.455987233623899257, -149.0115311668978393 ) ) ;
#71463=DIRECTION ( 'NONE',  ( 0.000000000000000000, -1.000000000000000000, 0.000000000000000000 ) ) ;
#71721=ORIENTED_EDGE ( 'NONE', *, *, #254431, .F. ) ;
#72142=DIRECTION ( 'NONE',  ( 0.000000000000000000, 0.000000000000000000, -1.000000000000000000 ) ) ;
#72263=EDGE_CURVE ( 'NONE', #138091, #107290, #107892, .T. ) ;
#72325=LINE ( 'NONE', #134819, #161894 ) ;
#72412=EDGE_LOOP ( 'NONE', ( #98745, #7828, #383, #57922, #22672, #202648, #205328, #92835, #250013 ) ) ;
#72416=DIRECTION ( 'NONE',  ( -1.073024830501117725E-15, 0.000000000000000000, 1.000000000000000000 ) ) ;
#72513=CARTESIAN_POINT ( 'NONE',  ( -16.87683809663750978, 9.950000000011137047, -147.4023640181965220 ) ) ;
#72683=DIRECTION ( 'NONE',  ( 1.073024830501117725E-15, -0.000000000000000000, -1.000000000000000000 ) ) ;
#72768=LINE ( 'NONE', #36190, #37356 ) ;
#72829=CARTESIAN_POINT ( 'NONE',  ( 20.05000000000002913, 7.250000000011171508, -154.8500000000000227 ) ) ;
#73030=CARTESIAN_POINT ( 'NONE',  ( -18.39999999999999858, 11.47316190337362762, -143.3259460668079726 ) ) ;
#73032=LINE ( 'NONE', #170868, #170191 ) ;
#73278=CARTESIAN_POINT ( 'NONE',  ( -18.40000000000000213, 8.822561741677553471, -143.2500000000000284 ) ) ;
#73538=AXIS2_PLACEMENT_3D ( 'NONE', #70437, #211191, #52098 ) ;
#73562=CARTESIAN_POINT ( 'NONE',  ( -15.75000000000000355, 9.850000000011133849, -150.7500000000000284 ) ) ;
#73602=CARTESIAN_POINT ( 'NONE',  ( 22.88900146558018989, 8.703904791123973084, -154.8500000000000227 ) ) ;
#74065=FACE_OUTER_BOUND ( 'NONE', #9161, .T. ) ;
#74096=CARTESIAN_POINT ( 'NONE',  ( -16.97048361161167662, 9.950000000011137047, -154.3588843444304075 ) ) ;
#74143=LINE ( 'NONE', #153707, #147007 ) ;
#74201=FACE_OUTER_BOUND ( 'NONE', #193229, .T. ) ;
#74270=VECTOR ( 'NONE', #44403, 1000.000000000000000 ) ;
#74375=AXIS2_PLACEMENT_3D ( 'NONE', #248174, #185632, #145205 ) ;
#74420=CARTESIAN_POINT ( 'NONE',  ( -21.65000000000000213, 7.250000000011139534, -146.6500000000000341 ) ) ;
#74463=VECTOR ( 'NONE', #216288, 1000.000000000000000 ) ;
#74504=LINE ( 'NONE', #131864, #205572 ) ;
#74536=PLANE ( 'NONE',  #142809 ) ;
#74652=DIRECTION ( 'NONE',  ( -0.000000000000000000, -0.000000000000000000, -1.000000000000000000 ) ) ;
#74810=ADVANCED_FACE ( 'NONE', ( #97834 ), #177441, .F. ) ;
#74951=CARTESIAN_POINT ( 'NONE',  ( -16.96982749440706328, 9.950000000011137047, -154.3752215911892733 ) ) ;
#74979=DIRECTION ( 'NONE',  ( -1.000000000000000000, -1.646408749285562691E-14, 1.073024830501117725E-15 ) ) ;
#75018=ADVANCED_FACE ( 'NONE', ( #134101 ), #149728, .T. ) ;
#75122=ORIENTED_EDGE ( 'NONE', *, *, #187254, .F. ) ;
#75547=DIRECTION ( 'NONE',  ( 0.000000000000000000, -1.000000000000000000, 0.000000000000000000 ) ) ;
#75725=CARTESIAN_POINT ( 'NONE',  ( -16.91256925476571382, 9.985731158139332209, -146.5323575109947569 ) ) ;
#75814=CARTESIAN_POINT ( 'NONE',  ( -16.93658211146644987, 9.994108662352344297, -154.9042950699557082 ) ) ;
#75816=DIRECTION ( 'NONE',  ( 1.000000000000000000, 0.000000000000000000, 1.073024830501117725E-15 ) ) ;
#75847=ORIENTED_EDGE ( 'NONE', *, *, #120416, .T. ) ;
#75984=EDGE_LOOP ( 'NONE', ( #151802, #240276 ) ) ;
#76217=CARTESIAN_POINT ( 'NONE',  ( 20.73486653747088226, 7.250000000011182166, -146.6500000000000341 ) ) ;
#76266=CARTESIAN_POINT ( 'NONE',  ( -18.40000000000000213, 11.33174054713633261, -154.8500000000000227 ) ) ;
#76274=ORIENTED_EDGE ( 'NONE', *, *, #63862, .F. ) ;
#76639=ORIENTED_EDGE ( 'NONE', *, *, #85825, .T. ) ;
#76709=ORIENTED_EDGE ( 'NONE', *, *, #39455, .F. ) ;
#76936=CARTESIAN_POINT ( 'NONE',  ( -16.94445028196807002, 9.992063609708893068, -154.8926698215815634 ) ) ;
#77049=EDGE_CURVE ( 'NONE', #81086, #256073, #28128, .T. ) ;
#77090=CARTESIAN_POINT ( 'NONE',  ( 18.39999999999999503, 5.650000000011139001, -154.8500000000000227 ) ) ;
#77329=CARTESIAN_POINT ( 'NONE',  ( 21.72449340488910607, 10.28395627750227703, -143.2500000000000284 ) ) ;
#77391=DIRECTION ( 'NONE',  ( 1.020425574104004196E-15, 1.210927747993693964E-31, 1.000000000000000000 ) ) ;
#77402=CARTESIAN_POINT ( 'NONE',  ( -17.71734398241073194, 10.84235722847571459, -157.2251382530056674 ) ) ;
#77446=AXIS2_PLACEMENT_3D ( 'NONE', #127943, #104490, #5387 ) ;
#77661=ORIENTED_EDGE ( 'NONE', *, *, #150498, .T. ) ;
#77992=EDGE_LOOP ( 'NONE', ( #57827, #99566, #127818, #24814 ) ) ;
#78064=CARTESIAN_POINT ( 'NONE',  ( 18.39999999999999503, 5.650000000011139001, -154.8500000000000227 ) ) ;
#78171=CARTESIAN_POINT ( 'NONE',  ( -21.64999999999999858, 9.350000000011133849, -154.8500000000000227 ) ) ;
#78300=CARTESIAN_POINT ( 'NONE',  ( 23.24999999999999645, 5.650000000011139001, -154.8500000000000227 ) ) ;
#78334=EDGE_CURVE ( 'NONE', #11462, #62456, #143855, .T. ) ;
#78680=ORIENTED_EDGE ( 'NONE', *, *, #224172, .F. ) ;
#78751=AXIS2_PLACEMENT_3D ( 'NONE', #151128, #69032, #187697 ) ;
#78753=CARTESIAN_POINT ( 'NONE',  ( -16.82542659449977762, 9.934499891438612451, -154.7553643999740416 ) ) ;
#78870=CARTESIAN_POINT ( 'NONE',  ( -12.25000000000000533, 9.350000000011133849, -150.8657431672739335 ) ) ;
#79144=CARTESIAN_POINT ( 'NONE',  ( -16.77683809663752257, 9.945835743215301505, -146.6639490191042228 ) ) ;
#79380=CARTESIAN_POINT ( 'NONE',  ( 18.39999999999997371, 11.75000000001113953, -143.2500000000000284 ) ) ;
#79631=LINE ( 'NONE', #159216, #39863 ) ;
#79744=ORIENTED_EDGE ( 'NONE', *, *, #35478, .T. ) ;
#79759=CARTESIAN_POINT ( 'NONE',  ( -16.87036670365548474, 9.989418819312804843, -154.9795601173020714 ) ) ;
#79818=ORIENTED_EDGE ( 'NONE', *, *, #251041, .T. ) ;
#79968=EDGE_CURVE ( 'NONE', #209017, #118840, #198721, .T. ) ;
#80038=ORIENTED_EDGE ( 'NONE', *, *, #162024, .T. ) ;
#80066=DIRECTION ( 'NONE',  ( 0.000000000000000000, 0.000000000000000000, -1.000000000000000000 ) ) ;
#81086=VERTEX_POINT ( 'NONE', #113516 ) ;
#81305=EDGE_CURVE ( 'NONE', #201469, #62456, #24718, .T. ) ;
#81350=EDGE_LOOP ( 'NONE', ( #89015, #91506, #203195, #62048, #168385, #158099, #248183, #188028, #237585, #163326, #123569, #76274, #97993, #99376 ) ) ;
#81389=VECTOR ( 'NONE', #200217, 1000.000000000000000 ) ;
#81429=VERTEX_POINT ( 'NONE', #72829 ) ;
#81458=CARTESIAN_POINT ( 'NONE',  ( -16.83199030136658081, 9.930648033124622742, -146.7724010226574762 ) ) ;
#81583=( NAMED_UNIT ( * ) PLANE_ANGLE_UNIT ( ) SI_UNIT ( $, .RADIAN. ) );
#81862=VERTEX_POINT ( 'NONE', #129859 ) ;
#82045=CARTESIAN_POINT ( 'NONE',  ( -16.86379686415369861, 9.975217759264314310, -146.5666101109097497 ) ) ;
#82240=ORIENTED_EDGE ( 'NONE', *, *, #138283, .F. ) ;
#82265=CARTESIAN_POINT ( 'NONE',  ( -16.93388492042259230, 9.988541822527057690, -146.5994548768138372 ) ) ;
#82298=FILL_AREA_STYLE ('',( #219262 ) ) ;
#82313=CARTESIAN_POINT ( 'NONE',  ( 12.24999999999999822, 9.350000000011139178, -150.5215193718251498 ) ) ;
#82316=CARTESIAN_POINT ( 'NONE',  ( -21.65000000000000213, 10.05000000001113847, -154.8500000000000227 ) ) ;
#82375=FACE_OUTER_BOUND ( 'NONE', #233297, .T. ) ;
#82415=ORIENTED_EDGE ( 'NONE', *, *, #234988, .F. ) ;
#82560=EDGE_CURVE ( 'NONE', #7029, #206656, #225779, .T. ) ;
#82984=ORIENTED_EDGE ( 'NONE', *, *, #165463, .F. ) ;
#83076=CARTESIAN_POINT ( 'NONE',  ( -16.78493211734303614, 9.945835743215324598, -154.8360509808959478 ) ) ;
#83125=CARTESIAN_POINT ( 'NONE',  ( -16.94333152886235894, 9.990342011461637028, -146.6079684689456144 ) ) ;
#83264=VERTEX_POINT ( 'NONE', #5782 ) ;
#83580=CARTESIAN_POINT ( 'NONE',  ( -17.22767730082391680, 10.34924421247984583, -145.3575713094252819 ) ) ;
#84129=( NAMED_UNIT ( * ) PLANE_ANGLE_UNIT ( ) SI_UNIT ( $, .RADIAN. ) );
#84262=EDGE_CURVE ( 'NONE', #252467, #171058, #187728, .T. ) ;
#84334=FACE_OUTER_BOUND ( 'NONE', #92610, .T. ) ;
#84394=CARTESIAN_POINT ( 'NONE',  ( -16.89268316805466341, 9.951721813253341153, -146.6442475214544743 ) ) ;
#84409=VECTOR ( 'NONE', #39265, 1000.000000000000000 ) ;
#84462=EDGE_CURVE ( 'NONE', #55215, #206656, #89548, .T. ) ;
#84856=SURFACE_SIDE_STYLE ('',( #204830 ) ) ;
#84873=LINE ( 'NONE', #82316, #184583 ) ;
#84966=CARTESIAN_POINT ( 'NONE',  ( 18.39999999999999503, 5.650000000011139001, -158.2500000000000284 ) ) ;
#84986=CARTESIAN_POINT ( 'NONE',  ( -16.85697194749123540, 9.908543714134728120, -146.9350042676138628 ) ) ;
#85051=ORIENTED_EDGE ( 'NONE', *, *, #175806, .F. ) ;
#85317=CARTESIAN_POINT ( 'NONE',  ( -16.87683809663753465, 9.864913778549572854, -147.2757156356385622 ) ) ;
#85427=CARTESIAN_POINT ( 'NONE',  ( -16.87383368123029825, 9.950000000011138823, -146.6500000000000341 ) ) ;
#85476=CARTESIAN_POINT ( 'NONE',  ( 15.39170923737819585, 9.389529397477897277, -151.8171079128937890 ) ) ;
#85647=B_SPLINE_CURVE_WITH_KNOTS ( 'NONE', 3,
 ( #53425, #15618, #132980, #149985, #250341, #112139, #194251, #95120, #191692, #113404 ),
 .UNSPECIFIED., .F., .F.,
 ( 4, 3, 3, 4 ),
 ( -2.000561356219677529E-06, 0.000000000000000000, 1.787822682429502760E-05, 4.206475347090109142E-05 ),
 .UNSPECIFIED. ) ;
#85825=EDGE_CURVE ( 'NONE', #55215, #217779, #145423, .T. ) ;
#86069=AXIS2_PLACEMENT_3D ( 'NONE', #71051, #150571, #51429 ) ;
#86276=ORIENTED_EDGE ( 'NONE', *, *, #177993, .T. ) ;
#86277=CARTESIAN_POINT ( 'NONE',  ( -16.89935556175703368, 9.950000000011137047, -147.1396763628858082 ) ) ;
#86344=ORIENTED_EDGE ( 'NONE', *, *, #49262, .F. ) ;
#86445=CARTESIAN_POINT ( 'NONE',  ( -18.39999999999999858, 11.47316190337362762, -143.2998292484660112 ) ) ;
#86604=CARTESIAN_POINT ( 'NONE',  ( -16.85312841634287295, 9.913606177331358182, -146.8971731332925685 ) ) ;
#86710=CARTESIAN_POINT ( 'NONE',  ( -16.98495255085919453, 10.00556436600593280, -154.8653827937795029 ) ) ;
#86721=AXIS2_PLACEMENT_3D ( 'NONE', #70465, #95122, #174712 ) ;
#86782=CARTESIAN_POINT ( 'NONE',  ( 12.84435279558020504, 9.410708747058237122, -152.0692084058441367 ) ) ;
#86865=EDGE_LOOP ( 'NONE', ( #66928, #19618, #35739, #162552 ) ) ;
#86940=CIRCLE ( 'NONE', #49564, 0.5000000000000004441 ) ;
#87290=STYLED_ITEM ( 'NONE', ( #65329 ), #112300 ) ;
#87398=CARTESIAN_POINT ( 'NONE',  ( -17.11825945287481332, 10.05000000001113847, -154.7500000000000284 ) ) ;
#87423=CARTESIAN_POINT ( 'NONE',  ( -17.11825945287482753, 9.950000000011138823, -146.7500000000000284 ) ) ;
#87674=CARTESIAN_POINT ( 'NONE',  ( 18.54999999999999716, 9.950000000011153034, -154.8500000000000796 ) ) ;
#87696=DIRECTION ( 'NONE',  ( 1.000000000000000000, -0.000000000000000000, -0.000000000000000000 ) ) ;
#87899=CARTESIAN_POINT ( 'NONE',  ( -17.11825945287482753, 10.05000000001113847, -146.7500000000000284 ) ) ;
#87962=CIRCLE ( 'NONE', #17278, 0.1999999999999987899 ) ;
#88054=CARTESIAN_POINT ( 'NONE',  ( 12.25000000000000178, 9.350000000011140955, -150.8642676076161138 ) ) ;
#88174=VECTOR ( 'NONE', #255907, 1000.000000000000000 ) ;
#88388=EDGE_LOOP ( 'NONE', ( #254441, #54657 ) ) ;
#88435=ORIENTED_EDGE ( 'NONE', *, *, #129617, .F. ) ;
#88480=CARTESIAN_POINT ( 'NONE',  ( -16.97092634996668181, 10.00088896635978486, -154.8698572337025325 ) ) ;
#88558=LINE ( 'NONE', #105537, #211223 ) ;
#88608=ORIENTED_EDGE ( 'NONE', *, *, #115274, .F. ) ;
#88823=VERTEX_POINT ( 'NONE', #57192 ) ;
#89015=ORIENTED_EDGE ( 'NONE', *, *, #142126, .F. ) ;
#89070=CARTESIAN_POINT ( 'NONE',  ( -16.86379686415369150, 9.975217759264314310, -154.9333898890903072 ) ) ;
#89077=ORIENTED_EDGE ( 'NONE', *, *, #188131, .T. ) ;
#89082=AXIS2_PLACEMENT_3D ( 'NONE', #171927, #251420, #212313 ) ;
#89185=ORIENTED_EDGE ( 'NONE', *, *, #138444, .F. ) ;
#89331=CARTESIAN_POINT ( 'NONE',  ( -16.97683809663752186, 9.950000000011137047, -154.0976359818037054 ) ) ;
#89401=EDGE_CURVE ( 'NONE', #1366, #70072, #209908, .T. ) ;
#89526=AXIS2_PLACEMENT_3D ( 'NONE', #146135, #148726, #4058 ) ;
#89548=LINE ( 'NONE', #169138, #4527 ) ;
#89730=CARTESIAN_POINT ( 'NONE',  ( 20.27550659511088682, 9.216043722520002035, -146.6500000000000341 ) ) ;
#90178=EDGE_LOOP ( 'NONE', ( #205012, #213837, #102681, #201844 ) ) ;
#90354=CARTESIAN_POINT ( 'NONE',  ( -16.86337532320261090, 9.979967204235514089, -154.9489244689828524 ) ) ;
#90379=CARTESIAN_POINT ( 'NONE',  ( -16.89268316805466341, 9.951721813253341153, -146.6442475214544743 ) ) ;
#90924=FACE_OUTER_BOUND ( 'NONE', #236599, .T. ) ;
#91022=CARTESIAN_POINT ( 'NONE',  ( 23.24999999999999645, 8.822561741677553471, -143.2500000000000284 ) ) ;
#91058=CARTESIAN_POINT ( 'NONE',  ( -16.97683809663752186, 9.950000000011138823, -154.0976359818037054 ) ) ;
#91086=ADVANCED_FACE ( 'NONE', ( #48791 ), #26688, .F. ) ;
#91243=ORIENTED_EDGE ( 'NONE', *, *, #49262, .T. ) ;
#91269=ORIENTED_EDGE ( 'NONE', *, *, #129776, .T. ) ;
#91334=FACE_BOUND ( 'NONE', #88388, .T. ) ;
#91400=ORIENTED_EDGE ( 'NONE', *, *, #2726, .T. ) ;
#91432=CARTESIAN_POINT ( 'NONE',  ( -16.86445178670583545, 9.962211629127152079, -146.6092225618827172 ) ) ;
#91488=DIRECTION ( 'NONE',  ( 0.000000000000000000, 0.000000000000000000, 1.000000000000000000 ) ) ;
#91506=ORIENTED_EDGE ( 'NONE', *, *, #235136, .F. ) ;
#91948=LINE ( 'NONE', #134898, #13372 ) ;
#92038=CARTESIAN_POINT ( 'NONE',  ( -17.29158576265543346, 10.36474766602906961, -156.0827582447921884 ) ) ;
#92055=CARTESIAN_POINT ( 'NONE',  ( 23.04999999999999716, 8.822561741677553471, -158.2500000000000284 ) ) ;
#92064=UNCERTAINTY_MEASURE_WITH_UNIT (LENGTH_MEASURE( 1.000000000000000082E-05 ), #241416, 'distance_accuracy_value', 'NONE');
#92136=ADVANCED_FACE ( 'NONE', ( #144058 ), #180644, .F. ) ;
#92254=CARTESIAN_POINT ( 'NONE',  ( -14.87779219673429054, 9.430633469083952392, -149.2317657948240992 ) ) ;
#92301=CYLINDRICAL_SURFACE ( 'NONE', #184302, 0.09999999999998898659 ) ;
#92592=DIRECTION ( 'NONE',  ( 1.000000000000000000, -0.000000000000000000, -0.000000000000000000 ) ) ;
#92610=EDGE_LOOP ( 'NONE', ( #30899, #138761, #19364, #227638 ) ) ;
#92794=PLANE ( 'NONE',  #207532 ) ;
#92835=ORIENTED_EDGE ( 'NONE', *, *, #111619, .T. ) ;
#92994=EDGE_CURVE ( 'NONE', #1028, #199629, #115290, .T. ) ;
#93186=DIRECTION ( 'NONE',  ( -0.000000000000000000, -0.000000000000000000, -1.000000000000000000 ) ) ;
#93498=LINE ( 'NONE', #212185, #136774 ) ;
#93624=CARTESIAN_POINT ( 'NONE',  ( -16.84419801905645997, 9.950000000011140600, -154.8305101537780502 ) ) ;
#93783=VERTEX_POINT ( 'NONE', #186920 ) ;
#93854=AXIS2_PLACEMENT_3D ( 'NONE', #92055, #38218, #29556 ) ;
#93856=ORIENTED_EDGE ( 'NONE', *, *, #227888, .F. ) ;
#93912=ORIENTED_EDGE ( 'NONE', *, *, #148686, .T. ) ;
#94014=LINE ( 'NONE', #78300, #162895 ) ;
#94046=CARTESIAN_POINT ( 'NONE',  ( -18.38817693311004575, 11.48149151591092476, -158.2500000000000284 ) ) ;
#94223=AXIS2_PLACEMENT_3D ( 'NONE', #29520, #127303, #71199 ) ;
#94396=CARTESIAN_POINT ( 'NONE',  ( -23.25000000000000355, 9.950000000011138823, -143.2500000000000284 ) ) ;
#94522=ORIENTED_EDGE ( 'NONE', *, *, #176278, .F. ) ;
#94586=FACE_OUTER_BOUND ( 'NONE', #5244, .T. ) ;
#94724=AXIS2_PLACEMENT_3D ( 'NONE', #51656, #210758, #12584 ) ;
#95012=ADVANCED_FACE ( 'NONE', ( #233779 ), #51246, .F. ) ;
#95120=CARTESIAN_POINT ( 'NONE',  ( -16.80117486205003630, 9.949657268323468529, -154.8488548729255285 ) ) ;
#95122=DIRECTION ( 'NONE',  ( -0.000000000000000000, -0.000000000000000000, -1.000000000000000000 ) ) ;
#95288=VECTOR ( 'NONE', #170270, 1000.000000000000000 ) ;
#95583=CARTESIAN_POINT ( 'NONE',  ( -16.97048326478264713, 9.950000000011137047, -147.1411068801272108 ) ) ;
#95594=LINE ( 'NONE', #21226, #201279 ) ;
#95698=ORIENTED_EDGE ( 'NONE', *, *, #175806, .T. ) ;
#95732=ORIENTED_EDGE ( 'NONE', *, *, #111877, .F. ) ;
#95962=EDGE_CURVE ( 'NONE', #201469, #43558, #218698, .T. ) ;
#96098=CARTESIAN_POINT ( 'NONE',  ( -15.75000000000000355, 9.350000000011140955, -150.7500000000000284 ) ) ;
#96111=EDGE_CURVE ( 'NONE', #136679, #166383, #51667, .T. ) ;
#96173=DIRECTION ( 'NONE',  ( -1.000000000000000000, 0.000000000000000000, 0.000000000000000000 ) ) ;
#96268=PLANE ( 'NONE',  #103302 ) ;
#96443=LINE ( 'NONE', #78171, #13274 ) ;
#96451=CARTESIAN_POINT ( 'NONE',  ( -16.97683809663752186, 9.850000000011137402, -154.0976359818037054 ) ) ;
#96623=CARTESIAN_POINT ( 'NONE',  ( -16.93344882324368683, 9.996588767299030565, -154.9130256948049578 ) ) ;
#96713=DIRECTION ( 'NONE',  ( -1.000000000000000000, -0.000000000000000000, 1.073024830501117725E-15 ) ) ;
#97287=ORIENTED_EDGE ( 'NONE', *, *, #66648, .T. ) ;
#97497=CARTESIAN_POINT ( 'NONE',  ( -14.00000000000000178, 9.850000000011133849, -150.7500000000000284 ) ) ;
#97564=CARTESIAN_POINT ( 'NONE',  ( -14.00000000000000178, 9.850000000011133849, -150.7500000000000284 ) ) ;
#97605=LINE ( 'NONE', #78064, #146756 ) ;
#97783=AXIS2_PLACEMENT_3D ( 'NONE', #44949, #226118, #245718 ) ;
#97834=FACE_OUTER_BOUND ( 'NONE', #101481, .T. ) ;
#97894=ORIENTED_EDGE ( 'NONE', *, *, #72263, .F. ) ;
#97915=AXIS2_PLACEMENT_3D ( 'NONE', #191193, #128635, #98134 ) ;
#97993=ORIENTED_EDGE ( 'NONE', *, *, #235401, .F. ) ;
#98033=CARTESIAN_POINT ( 'NONE',  ( -17.73285935862336515, 10.85798180379888223, -157.2585618097758982 ) ) ;
#98098=( BOUNDED_CURVE ( )  B_SPLINE_CURVE ( 3, ( #99323, #1521, #118933, #161918 ),
 .UNSPECIFIED., .F., .F. ) 
 B_SPLINE_CURVE_WITH_KNOTS ( ( 4, 4 ),
 ( 4.712388980384689674, 5.672655318024514060 ),
 .UNSPECIFIED. ) 
 CURVE ( )  GEOMETRIC_REPRESENTATION_ITEM ( )  RATIONAL_B_SPLINE_CURVE ( ( 1.000000000000000000, 0.9246222802177627154, 0.9246222802177627154, 1.000000000000000000 ) ) 
 REPRESENTATION_ITEM ( '' )  );
#98134=DIRECTION ( 'NONE',  ( 1.000000000000000000, 0.000000000000000000, -0.000000000000000000 ) ) ;
#98293=CARTESIAN_POINT ( 'NONE',  ( -16.89935556175702303, 9.950000000011135270, -154.3603236371143055 ) ) ;
#98354=CARTESIAN_POINT ( 'NONE',  ( -21.65000000000000213, 9.950000000011140600, -146.6500000000000341 ) ) ;
#98658=DIRECTION ( 'NONE',  ( 0.000000000000000000, 0.000000000000000000, 1.000000000000000000 ) ) ;
#98745=ORIENTED_EDGE ( 'NONE', *, *, #126868, .T. ) ;
#98840=PLANE ( 'NONE',  #247301 ) ;
#99323=CARTESIAN_POINT ( 'NONE',  ( -17.11825945287482753, 10.05000000001113847, -146.6500000000000341 ) ) ;
#99376=ORIENTED_EDGE ( 'NONE', *, *, #177641, .F. ) ;
#99490=ORIENTED_EDGE ( 'NONE', *, *, #222848, .F. ) ;
#99522=CARTESIAN_POINT ( 'NONE',  ( -17.22361732159831504, 10.34515565861358866, -156.1292154741328773 ) ) ;
#99566=ORIENTED_EDGE ( 'NONE', *, *, #110894, .T. ) ;
#99863=ORIENTED_EDGE ( 'NONE', *, *, #170197, .T. ) ;
#99865=PRESENTATION_STYLE_ASSIGNMENT (( #218540 ) ) ;
#99956=LINE ( 'NONE', #176990, #177897 ) ;
#99977=CARTESIAN_POINT ( 'NONE',  ( -16.77902162784673834, 9.946419257218995114, -146.6619912440693554 ) ) ;
#100369=CARTESIAN_POINT ( 'NONE',  ( -18.40000000000000213, 11.48667500176882328, -143.2500000000000284 ) ) ;
#100926=PLANE ( 'NONE',  #156677 ) ;
#100974=CARTESIAN_POINT ( 'NONE',  ( -15.66061380678752180, 9.360723793997191677, -151.3139271946067481 ) ) ;
#101121=CARTESIAN_POINT ( 'NONE',  ( -16.88560720703333473, 9.950564843760847822, -146.6481119208637551 ) ) ;
#101129=EDGE_CURVE ( 'NONE', #71313, #220835, #188038, .T. ) ;
#101481=EDGE_LOOP ( 'NONE', ( #27123, #255072, #207004 ) ) ;
#101511=DIRECTION ( 'NONE',  ( -0.000000000000000000, 1.000000000000000000, -0.000000000000000000 ) ) ;
#101621=CARTESIAN_POINT ( 'NONE',  ( 18.39999999999999503, 8.822561741677553471, -158.2500000000000284 ) ) ;
#101832=CARTESIAN_POINT ( 'NONE',  ( -16.95709691156916321, 9.950000000011137047, -146.6600575625134297 ) ) ;
#101874=FACE_OUTER_BOUND ( 'NONE', #58927, .T. ) ;
#101941=CYLINDRICAL_SURFACE ( 'NONE', #17734, 0.1000000000000013656 ) ;
#102300=CARTESIAN_POINT ( 'NONE',  ( -16.80100426158789872, 9.943150520407289861, -146.6829457528340299 ) ) ;
#102314=DIRECTION ( 'NONE',  ( 1.000000000000000000, 0.000000000000000000, -0.000000000000000000 ) ) ;
#102404=ADVANCED_FACE ( 'NONE', ( #180280 ), #134707, .F. ) ;
#102429=SURFACE_STYLE_FILL_AREA ( #240696 ) ;
#102465=ORIENTED_EDGE ( 'NONE', *, *, #46324, .F. ) ;
#102479=CARTESIAN_POINT ( 'NONE',  ( 14.88075390448864255, 9.431689550535255151, -152.2792900322359912 ) ) ;
#102551=FACE_OUTER_BOUND ( 'NONE', #117349, .T. ) ;
#102653=CARTESIAN_POINT ( 'NONE',  ( -16.87372397896795562, 9.880599536652891146, -154.3507245100357750 ) ) ;
#102681=ORIENTED_EDGE ( 'NONE', *, *, #95962, .T. ) ;
#103173=CARTESIAN_POINT ( 'NONE',  ( 12.25000000000000000, 9.350000000011140955, -150.7500000000000284 ) ) ;
#103183=DIRECTION ( 'NONE',  ( -0.000000000000000000, -0.000000000000000000, -1.000000000000000000 ) ) ;
#103302=AXIS2_PLACEMENT_3D ( 'NONE', #231973, #191568, #254065 ) ;
#103461=EDGE_LOOP ( 'NONE', ( #211947, #148986, #156643, #78680 ) ) ;
#103498=EDGE_CURVE ( 'NONE', #123340, #221, #202155, .T. ) ;
#103528=CARTESIAN_POINT ( 'NONE',  ( -20.65000000000000568, 5.650000000011139001, -143.2500000000000284 ) ) ;
#103569=CARTESIAN_POINT ( 'NONE',  ( -15.75000000000000355, 9.350000000011139178, -150.8642676076160569 ) ) ;
#103596=VERTEX_POINT ( 'NONE', #116800 ) ;
#103626=ORIENTED_EDGE ( 'NONE', *, *, #165463, .T. ) ;
#103687=DIRECTION ( 'NONE',  ( -0.000000000000000000, -0.000000000000000000, -1.000000000000000000 ) ) ;
#103769=CARTESIAN_POINT ( 'NONE',  ( 15.73863059295127798, 9.351403174152812525, -150.9795304368385302 ) ) ;
#103871=AXIS2_PLACEMENT_3D ( 'NONE', #234813, #140853, #220396 ) ;
#103981=FACE_OUTER_BOUND ( 'NONE', #86865, .T. ) ;
#104320=ADVANCED_FACE ( 'NONE', ( #41200 ), #141547, .T. ) ;
#104451=DIRECTION ( 'NONE',  ( -1.000000000000000000, 0.000000000000000000, -0.000000000000000000 ) ) ;
#104490=DIRECTION ( 'NONE',  ( 1.186688945009010077E-16, -1.000000000000000000, -0.000000000000000000 ) ) ;
#104725=EDGE_CURVE ( 'NONE', #127092, #123340, #145088, .T. ) ;
#104870=ADVANCED_FACE ( 'NONE', ( #151556 ), #29054, .F. ) ;
#105232=ADVANCED_FACE ( 'NONE', ( #48265 ), #28757, .F. ) ;
#105526=CARTESIAN_POINT ( 'NONE',  ( 18.39999999999999503, 11.75000000001113953, -154.8500000000000227 ) ) ;
#105537=CARTESIAN_POINT ( 'NONE',  ( -16.87683809663752399, 9.850000000011140955, -146.6500000000000341 ) ) ;
#105571=CARTESIAN_POINT ( 'NONE',  ( -18.40000000000000213, 11.75000000001113953, -146.6500000000000341 ) ) ;
#105724=CARTESIAN_POINT ( 'NONE',  ( -21.65000000000000213, 7.250000000011138646, -143.2500000000000284 ) ) ;
#105826=CARTESIAN_POINT ( 'NONE',  ( -18.40000000000000213, 11.75000000001113953, -154.8500000000000227 ) ) ;
#105833=PLANE ( 'NONE',  #255513 ) ;
#105837=CARTESIAN_POINT ( 'NONE',  ( -16.94333152882356330, 9.990342011468825945, -154.8920315311015088 ) ) ;
#105842=CARTESIAN_POINT ( 'NONE',  ( -16.79270642812298320, 9.946244216949343908, -146.6610667214371233 ) ) ;
#105849=DIRECTION ( 'NONE',  ( 1.000000000000000000, 1.646408749285562691E-14, 1.073024830501117725E-15 ) ) ;
#106146=CARTESIAN_POINT ( 'NONE',  ( -15.55912972643741199, 8.490870273573719373, -146.6500000000000341 ) ) ;
#106232=FACE_OUTER_BOUND ( 'NONE', #211591, .T. ) ;
#106281=ADVANCED_FACE ( 'NONE', ( #206102 ), #223053, .T. ) ;
#106314=ORIENTED_EDGE ( 'NONE', *, *, #129940, .T. ) ;
#106338=CARTESIAN_POINT ( 'NONE',  ( 14.22916352759893854, 9.457410930301318075, -152.4999159087463170 ) ) ;
#106398=LINE ( 'NONE', #185963, #17241 ) ;
#106629=ORIENTED_EDGE ( 'NONE', *, *, #115787, .F. ) ;
#106917=CARTESIAN_POINT ( 'NONE',  ( 15.74999999999999645, 9.850000000011137402, -150.7500000000000284 ) ) ;
#106933=DIRECTION ( 'NONE',  ( 1.000000000000000000, 0.000000000000000000, 0.000000000000000000 ) ) ;
#107025=CARTESIAN_POINT ( 'NONE',  ( 13.88302573338718737, 9.457410944778565920, -149.0000839737900549 ) ) ;
#107125=FACE_OUTER_BOUND ( 'NONE', #159201, .T. ) ;
#107176=CARTESIAN_POINT ( 'NONE',  ( -16.88853107394619002, 9.950878483358135185, -154.8529363468922497 ) ) ;
#107202=AXIS2_PLACEMENT_3D ( 'NONE', #113368, #11720, #75547 ) ;
#107220=ADVANCED_FACE ( 'NONE', ( #101874 ), #2784, .F. ) ;
#107290=VERTEX_POINT ( 'NONE', #221821 ) ;
#107463=LINE ( 'NONE', #5767, #196539 ) ;
#107534=ORIENTED_EDGE ( 'NONE', *, *, #193973, .F. ) ;
#107646=CARTESIAN_POINT ( 'NONE',  ( 12.48201962039795987, 9.376659938544689155, -151.6281925482172994 ) ) ;
#107803=CARTESIAN_POINT ( 'NONE',  ( -18.40000000000000213, 5.650000000011139001, -154.8500000000000227 ) ) ;
#107892=LINE ( 'NONE', #66208, #210764 ) ;
#107961=CARTESIAN_POINT ( 'NONE',  ( -18.40000000000000213, 11.75000000001113953, -154.8500000000000227 ) ) ;
#108047=( BOUNDED_CURVE ( )  B_SPLINE_CURVE ( 3, ( #171453, #86710, #26795, #108868 ),
 .UNSPECIFIED., .F., .F. ) 
 B_SPLINE_CURVE_WITH_KNOTS ( ( 4, 4 ),
 ( 3.752122642744872394, 4.712388980384671910 ),
 .UNSPECIFIED. ) 
 CURVE ( )  GEOMETRIC_REPRESENTATION_ITEM ( )  RATIONAL_B_SPLINE_CURVE ( ( 1.000000000000000000, 0.9246222802177666011, 0.9246222802177666011, 1.000000000000000000 ) ) 
 REPRESENTATION_ITEM ( '' )  );
#108132=VECTOR ( 'NONE', #156536, 1000.000000000000000 ) ;
#108135=VECTOR ( 'NONE', #113543, 1000.000000000000000 ) ;
#108434=CARTESIAN_POINT ( 'NONE',  ( -16.94389599337536012, 9.991197989767877985, -154.8923551982016420 ) ) ;
#108736=LINE ( 'NONE', #106146, #133280 ) ;
#108868=CARTESIAN_POINT ( 'NONE',  ( -17.11825945287481332, 10.05000000001113847, -154.8500000000000227 ) ) ;
#108905=CARTESIAN_POINT ( 'NONE',  ( -16.87683809663752399, 9.850000000011139178, -154.0976359818037054 ) ) ;
#109144=CARTESIAN_POINT ( 'NONE',  ( -16.93970660449832977, 10.01284139164673270, -146.5522817357944803 ) ) ;
#109166=ORIENTED_EDGE ( 'NONE', *, *, #161250, .T. ) ;
#109202=AXIS2_PLACEMENT_3D ( 'NONE', #55655, #174415, #218599 ) ;
#109708=LINE ( 'NONE', #228404, #233588 ) ;
#109773=CARTESIAN_POINT ( 'NONE',  ( -21.65000000000000213, 7.250000000011139534, -154.8500000000000227 ) ) ;
#110868=ADVANCED_FACE ( 'NONE', ( #15620 ), #212523, .T. ) ;
#110894=EDGE_CURVE ( 'NONE', #199629, #184760, #73032, .T. ) ;
#111001=CARTESIAN_POINT ( 'NONE',  ( -16.89268316805465986, 9.951721813253337601, -154.8557524785455541 ) ) ;
#111044=DIRECTION ( 'NONE',  ( 1.000000000000000000, 0.000000000000000000, -0.000000000000000000 ) ) ;
#111216=CARTESIAN_POINT ( 'NONE',  ( -16.87786941232801396, 9.958154714156124854, -154.8771857997940060 ) ) ;
#111563=EDGE_LOOP ( 'NONE', ( #182184, #66858 ) ) ;
#111582=ORIENTED_EDGE ( 'NONE', *, *, #170197, .F. ) ;
#111619=EDGE_CURVE ( 'NONE', #221938, #207052, #112772, .T. ) ;
#111705=CARTESIAN_POINT ( 'NONE',  ( -17.11825945287481332, 9.950000000011138823, -154.7500000000000284 ) ) ;
#111834=( BOUNDED_CURVE ( )  B_SPLINE_CURVE ( 3, ( #146040, #66523, #207329, #28721 ),
 .UNSPECIFIED., .F., .F. ) 
 B_SPLINE_CURVE_WITH_KNOTS ( ( 4, 4 ),
 ( 1.570796326794885012, 3.141592653589794448 ),
 .UNSPECIFIED. ) 
 CURVE ( )  GEOMETRIC_REPRESENTATION_ITEM ( )  RATIONAL_B_SPLINE_CURVE ( ( 1.000000000000000000, 0.8047378541243619399, 0.8047378541243619399, 1.000000000000000000 ) ) 
 REPRESENTATION_ITEM ( '' )  );
#111841=CARTESIAN_POINT ( 'NONE',  ( -13.88555196119803625, 9.457431528860070102, -148.9999169378996555 ) ) ;
#111877=EDGE_CURVE ( 'NONE', #135886, #23667, #124511, .T. ) ;
#112139=CARTESIAN_POINT ( 'NONE',  ( -16.78805706634180339, 9.948252493082335945, -154.8441532080318837 ) ) ;
#112300=MANIFOLD_SOLID_BREP ( 'Stock-MAS-200-1', #199013 ) ;
#112338=CARTESIAN_POINT ( 'NONE',  ( -16.89081410710458542, 9.951318529858268036, -154.8544059198364096 ) ) ;
#112571=DIRECTION ( 'NONE',  ( -1.000000000000000000, 0.000000000000000000, 0.000000000000000000 ) ) ;
#112772=LINE ( 'NONE', #107961, #162152 ) ;
#113067=CARTESIAN_POINT ( 'NONE',  ( 20.99999999999999645, 9.750000000011137757, -154.8500000000000227 ) ) ;
#113115=CARTESIAN_POINT ( 'NONE',  ( -15.75000000000000000, 9.350000000011140955, -150.5215193718251214 ) ) ;
#113368=CARTESIAN_POINT ( 'NONE',  ( -21.64999999999999858, 10.05000000001113847, -154.7500000000000284 ) ) ;
#113404=CARTESIAN_POINT ( 'NONE',  ( -16.81744102076748959, 9.950000000011138823, -154.8500000000000227 ) ) ;
#113451=CYLINDRICAL_SURFACE ( 'NONE', #132095, 14.30833333333333890 ) ;
#113473=DIRECTION ( 'NONE',  ( 0.000000000000000000, 1.000000000000000000, 0.000000000000000000 ) ) ;
#113516=CARTESIAN_POINT ( 'NONE',  ( -16.87036670365548474, 9.989418819312801290, -154.9795601173020714 ) ) ;
#113543=DIRECTION ( 'NONE',  ( 1.000000000000000000, 0.000000000000000000, 0.000000000000000000 ) ) ;
#113609=VECTOR ( 'NONE', #206697, 1000.000000000000000 ) ;
#113618=CARTESIAN_POINT ( 'NONE',  ( -18.38204789744325396, 11.47950103717623982, -158.2500000000000284 ) ) ;
#113630=EDGE_LOOP ( 'NONE', ( #88608, #107534, #37454, #214111 ) ) ;
#113719=CARTESIAN_POINT ( 'NONE',  ( 18.39999999999998082, 11.47316190337362585, -143.2500000000000284 ) ) ;
#114033=CARTESIAN_POINT ( 'NONE',  ( -16.88783316861808714, 9.950000000011137047, -154.7477359580207406 ) ) ;
#114186=CARTESIAN_POINT ( 'NONE',  ( -16.89155683852450807, 9.950000000011137047, -147.2773718495397475 ) ) ;
#114341=ORIENTED_EDGE ( 'NONE', *, *, #170993, .T. ) ;
#114469=CARTESIAN_POINT ( 'NONE',  ( -16.86133551771148831, 9.950000000011137047, -154.8013434345467090 ) ) ;
#114644=AXIS2_PLACEMENT_3D ( 'NONE', #157294, #116857, #158578 ) ;
#114878=MECHANICAL_DESIGN_GEOMETRIC_PRESENTATION_REPRESENTATION('',(#185604),#52312);
#114939=DIRECTION ( 'NONE',  ( -0.000000000000000000, 1.000000000000000000, 0.000000000000000000 ) ) ;
#115103=ORIENTED_EDGE ( 'NONE', *, *, #131192, .T. ) ;
#115155=CARTESIAN_POINT ( 'NONE',  ( -16.97683809663752186, 9.950000000011138823, -147.4023640181965220 ) ) ;
#115219=DIRECTION ( 'NONE',  ( -0.000000000000000000, -0.000000000000000000, -1.000000000000000000 ) ) ;
#115254=DIRECTION ( 'NONE',  ( 0.000000000000000000, -1.000000000000000000, 0.000000000000000000 ) ) ;
#115274=EDGE_CURVE ( 'NONE', #22565, #31535, #155670, .T. ) ;
#115290=CIRCLE ( 'NONE', #2854, 1.749999999999998002 ) ;
#115602=VERTEX_POINT ( 'NONE', #109773 ) ;
#115685=CARTESIAN_POINT ( 'NONE',  ( -15.52965525596987462, 9.375538102059163492, -149.8698758809908611 ) ) ;
#115787=EDGE_CURVE ( 'NONE', #190690, #93783, #217846, .T. ) ;
#116242=CARTESIAN_POINT ( 'NONE',  ( -16.93826681692523195, 10.01142872029886632, -154.9454584673594582 ) ) ;
#116256=EDGE_LOOP ( 'NONE', ( #204799, #70358, #225479, #95698, #66837, #14544, #195149, #64372, #235359 ) ) ;
#116447=CARTESIAN_POINT ( 'NONE',  ( -16.90137573187933384, 9.950000000011137047, -146.7884174240969628 ) ) ;
#116615=CARTESIAN_POINT ( 'NONE',  ( -16.80070461187903419, 9.950000000011137047, -154.8530361708395162 ) ) ;
#116725=CARTESIAN_POINT ( 'NONE',  ( -17.11825945287481687, 9.950000000011140600, -154.8500000000000227 ) ) ;
#116799=VECTOR ( 'NONE', #96713, 1000.000000000000000 ) ;
#116800=CARTESIAN_POINT ( 'NONE',  ( -18.40000000000000213, 11.47316190337364183, -154.9500000000000455 ) ) ;
#116857=DIRECTION ( 'NONE',  ( -0.000000000000000000, -0.000000000000000000, -1.000000000000000000 ) ) ;
#117146=B_SPLINE_CURVE_WITH_KNOTS ( 'NONE', 3,
 ( #84394, #221370, #205667, #27078, #117490, #223947, #201829, #83125, #204384, #162721 ),
 .UNSPECIFIED., .F., .F.,
 ( 4, 3, 3, 4 ),
 ( 1.886399917053072492E-15, 3.877043166999333273E-05, 7.336897548476527698E-05, 7.659383120239750958E-05 ),
 .UNSPECIFIED. ) ;
#117349=EDGE_LOOP ( 'NONE', ( #129004, #161353, #208614, #76639 ) ) ;
#117468=CARTESIAN_POINT ( 'NONE',  ( 15.74999999999999645, 9.850000000011137402, -150.7500000000000284 ) ) ;
#117490=CARTESIAN_POINT ( 'NONE',  ( -16.92925196614876171, 9.972331796421276096, -146.6167448477168023 ) ) ;
#117790=DIRECTION ( 'NONE',  ( 1.186688945009010077E-16, -1.000000000000000000, -0.000000000000000000 ) ) ;
#118111=AXIS2_PLACEMENT_3D ( 'NONE', #87398, #226921, #48283 ) ;
#118123=CARTESIAN_POINT ( 'NONE',  ( 16.87683809663749557, 9.950000000011131718, -154.8500000000000227 ) ) ;
#118166=CARTESIAN_POINT ( 'NONE',  ( -18.40000000000000213, 11.47316190337364183, -158.1740539331920559 ) ) ;
#118302=CARTESIAN_POINT ( 'NONE',  ( -16.81095280782810875, 9.950000000011138823, -146.6499999999991530 ) ) ;
#118667=CARTESIAN_POINT ( 'NONE',  ( -16.86337532320262156, 9.979967204235514089, -146.5510755310172044 ) ) ;
#118840=VERTEX_POINT ( 'NONE', #150300 ) ;
#118933=CARTESIAN_POINT ( 'NONE',  ( -16.98495255085921229, 10.00556436600593280, -146.6346172062204971 ) ) ;
#119192=CARTESIAN_POINT ( 'NONE',  ( -16.89155683852495926, 9.950000000011137047, -154.2226281504603662 ) ) ;
#119313=CARTESIAN_POINT ( 'NONE',  ( -15.31895204843004699, 9.396533993965073606, -151.9059397791733090 ) ) ;
#119383=CARTESIAN_POINT ( 'NONE',  ( -18.40000000000000213, 11.47316190337362762, -146.5500000000000114 ) ) ;
#119698=CIRCLE ( 'NONE', #107202, 0.09999999999999939493 ) ;
#120017=CARTESIAN_POINT ( 'NONE',  ( -16.92973740335288824, 9.992503814478434165, -154.9060590352028441 ) ) ;
#120214=VECTOR ( 'NONE', #168886, 1000.000000000000000 ) ;
#120241=CARTESIAN_POINT ( 'NONE',  ( -17.78241384944000103, 10.85557575281363896, -157.2509623275143724 ) ) ;
#120370=CARTESIAN_POINT ( 'NONE',  ( 18.39999999999999503, 11.47316190337363828, -146.6500000000000341 ) ) ;
#120416=EDGE_CURVE ( 'NONE', #115602, #9223, #96443, .T. ) ;
#120626=CARTESIAN_POINT ( 'NONE',  ( -18.39999999999999858, 11.47316190337362762, -143.3259460668079726 ) ) ;
#120706=EDGE_CURVE ( 'NONE', #166775, #209272, #10223, .T. ) ;
#120729=B_SPLINE_CURVE_WITH_KNOTS ( 'NONE', 3,
 ( #249237, #108434, #105837, #69321, #146262, #70622, #185401, #228390, #229668, #49738, #225785, #31495, #111001 ),
 .UNSPECIFIED., .F., .F.,
 ( 4, 3, 3, 3, 4 ),
 ( -3.224855718284247652E-06, 4.235164736271501695E-22, 6.199515528661409170E-06, 4.034952380126323066E-05, 7.452715123697944196E-05 ),
 .UNSPECIFIED. ) ;
#120732=ADVANCED_FACE ( 'NONE', ( #74065 ), #92301, .T. ) ;
#120755=EDGE_LOOP ( 'NONE', ( #88435, #149630, #13540, #160518, #17172 ) ) ;
#120756=LINE ( 'NONE', #183271, #228327 ) ;
#120776=( LENGTH_UNIT ( ) NAMED_UNIT ( * ) SI_UNIT ( .MILLI., .METRE. ) );
#120891=CARTESIAN_POINT ( 'NONE',  ( -16.79814274880124358, 9.949272542688458287, -146.6524330370480413 ) ) ;
#121030=ORIENTED_EDGE ( 'NONE', *, *, #130205, .F. ) ;
#121114=VERTEX_POINT ( 'NONE', #256137 ) ;
#121168=CARTESIAN_POINT ( 'NONE',  ( 18.39999999999999503, 11.75000000001113953, -158.2500000000000284 ) ) ;
#121252=CYLINDRICAL_SURFACE ( 'NONE', #140317, 1.749999999999999778 ) ;
#121495=CARTESIAN_POINT ( 'NONE',  ( -17.80356949364094277, 10.87673139701457536, -144.2869269757789823 ) ) ;
#121513=CARTESIAN_POINT ( 'NONE',  ( -17.22767730082509630, 10.34924421247947102, -156.1424286905735528 ) ) ;
#121613=CARTESIAN_POINT ( 'NONE',  ( -16.88705144915419964, 9.950000000011137047, -146.9309785947120304 ) ) ;
#121676=ORIENTED_EDGE ( 'NONE', *, *, #101129, .T. ) ;
#121884=CARTESIAN_POINT ( 'NONE',  ( -17.04295772865474490, 10.02489942527111388, -154.8500000000000227 ) ) ;
#121997=VECTOR ( 'NONE', #239904, 1000.000000000000000 ) ;
#121999=ORIENTED_EDGE ( 'NONE', *, *, #162024, .F. ) ;
#122778=CARTESIAN_POINT ( 'NONE',  ( 15.06592377766031454, 9.417789466963359502, -149.3573845439768775 ) ) ;
#123340=VERTEX_POINT ( 'NONE', #11977 ) ;
#123569=ORIENTED_EDGE ( 'NONE', *, *, #242423, .F. ) ;
#123876=EDGE_LOOP ( 'NONE', ( #125566, #25136, #165358, #232280 ) ) ;
#124043=CARTESIAN_POINT ( 'NONE',  ( -17.29838795458769596, 10.37154985796132500, -145.3952587173806705 ) ) ;
#124054=CARTESIAN_POINT ( 'NONE',  ( 12.29592348164039706, 9.355806591641284697, -150.2911025315461586 ) ) ;
#124146=ORIENTED_EDGE ( 'NONE', *, *, #92994, .T. ) ;
#124165=CARTESIAN_POINT ( 'NONE',  ( -16.87333278164158656, 9.882609784590076885, -147.1331678061536365 ) ) ;
#124323=CARTESIAN_POINT ( 'NONE',  ( -23.25000000000000355, 5.650000000011139001, -143.2500000000000284 ) ) ;
#124488=CARTESIAN_POINT ( 'NONE',  ( -16.87683809663752399, 9.850000000011144508, -147.4023640181963515 ) ) ;
#124511=B_SPLINE_CURVE_WITH_KNOTS ( 'NONE', 3,
 ( #4363, #86445, #66917, #25245 ),
 .UNSPECIFIED., .F., .F.,
 ( 4, 4 ),
 ( 0.000000000000000000, 7.713889350930799751E-05 ),
 .UNSPECIFIED. ) ;
#124529=DIRECTION ( 'NONE',  ( -1.073024830501117725E-15, 0.000000000000000000, -1.000000000000000000 ) ) ;
#124928=ORIENTED_EDGE ( 'NONE', *, *, #39455, .T. ) ;
#124947=LINE ( 'NONE', #244877, #45629 ) ;
#125443=CARTESIAN_POINT ( 'NONE',  ( -16.80070461187906261, 9.950000000011135270, -146.6469638291605975 ) ) ;
#125566=ORIENTED_EDGE ( 'NONE', *, *, #219747, .F. ) ;
#125677=CARTESIAN_POINT ( 'NONE',  ( -17.11825945287482753, 9.950000000011138823, -146.7500000000000284 ) ) ;
#125692=ADVANCED_FACE ( 'NONE', ( #140773 ), #121252, .F. ) ;
#125915=CARTESIAN_POINT ( 'NONE',  ( 15.69410316191959609, 9.356746017089404788, -151.2033597213642224 ) ) ;
#126121=CYLINDRICAL_SURFACE ( 'NONE', #6345, 0.09999999999999939493 ) ;
#126204=CARTESIAN_POINT ( 'NONE',  ( -16.97683809663752186, 9.950000000011138823, -154.0976359818037054 ) ) ;
#126258=ORIENTED_EDGE ( 'NONE', *, *, #115274, .T. ) ;
#126375=CARTESIAN_POINT ( 'NONE',  ( -23.25000000000000355, 11.75000000001113953, -154.8500000000000227 ) ) ;
#126492=LINE ( 'NONE', #106917, #74270 ) ;
#126493=EDGE_LOOP ( 'NONE', ( #124928, #241609, #255402, #43321, #49533, #62487, #197535, #52996, #86276, #142807, #4528, #229653, #210829, #203397, #2300, #50766, #167165, #224663 ) ) ;
#126568=CARTESIAN_POINT ( 'NONE',  ( -17.11825945287482753, 9.950000000011140600, -146.6500000000000341 ) ) ;
#126607=CARTESIAN_POINT ( 'NONE',  ( 15.15590539855246099, 9.410682294279107296, -149.4311434419482794 ) ) ;
#126704=DIRECTION ( 'NONE',  ( 0.000000000000000000, 1.000000000000000000, -0.000000000000000000 ) ) ;
#126717=AXIS2_PLACEMENT_3D ( 'NONE', #195774, #17133, #233601 ) ;
#126750=CARTESIAN_POINT ( 'NONE',  ( -16.88593481969334675, 9.950560090095464716, -154.8518722569445174 ) ) ;
#126868=EDGE_CURVE ( 'NONE', #45717, #141855, #149818, .T. ) ;
#127092=VERTEX_POINT ( 'NONE', #38847 ) ;
#127217=CARTESIAN_POINT ( 'NONE',  ( 12.60873083341397383, 9.389571634557567492, -151.8176407123691547 ) ) ;
#127303=DIRECTION ( 'NONE',  ( 0.2834754621636439431, -0.2834754621636535465, -0.9161240771326838450 ) ) ;
#127669=CARTESIAN_POINT ( 'NONE',  ( -17.11825945287482753, 10.05000000001113847, -146.6500000000000341 ) ) ;
#127818=ORIENTED_EDGE ( 'NONE', *, *, #173443, .F. ) ;
#127837=EDGE_CURVE ( 'NONE', #171058, #118840, #88558, .T. ) ;
#127943=CARTESIAN_POINT ( 'NONE',  ( 13.99999999999999822, 9.850000000011137402, -150.7500000000000284 ) ) ;
#128116=DIRECTION ( 'NONE',  ( 1.000000000000000000, 0.000000000000000000, -1.020425574104004196E-15 ) ) ;
#128259=ORIENTED_EDGE ( 'NONE', *, *, #159188, .F. ) ;
#128278=DIRECTION ( 'NONE',  ( -0.000000000000000000, -0.000000000000000000, -1.000000000000000000 ) ) ;
#128635=DIRECTION ( 'NONE',  ( 0.000000000000000000, 0.000000000000000000, 1.000000000000000000 ) ) ;
#128655=ORIENTED_EDGE ( 'NONE', *, *, #223145, .F. ) ;
#128731=VECTOR ( 'NONE', #87696, 1000.000000000000000 ) ;
#129004=ORIENTED_EDGE ( 'NONE', *, *, #61494, .T. ) ;
#129333=AXIS2_PLACEMENT_3D ( 'NONE', #240864, #163893, #239580 ) ;
#129382=DIRECTION ( 'NONE',  ( 0.000000000000000000, -1.000000000000000000, 0.000000000000000000 ) ) ;
#129394=CARTESIAN_POINT ( 'NONE',  ( -18.40000000000000213, 5.650000000011139001, -146.6500000000000341 ) ) ;
#129617=EDGE_CURVE ( 'NONE', #256073, #212672, #120756, .T. ) ;
#129669=VERTEX_POINT ( 'NONE', #161145 ) ;
#129776=EDGE_CURVE ( 'NONE', #156798, #198318, #247075, .T. ) ;
#129859=CARTESIAN_POINT ( 'NONE',  ( 21.72449340488909897, 10.28395627750227703, -154.8500000000000227 ) ) ;
#129940=EDGE_CURVE ( 'NONE', #207052, #180463, #72325, .T. ) ;
#130040=DIRECTION ( 'NONE',  ( 1.186688945009009831E-16, -1.000000000000000000, 0.000000000000000000 ) ) ;
#130205=EDGE_CURVE ( 'NONE', #10139, #59289, #169873, .T. ) ;
#130339=VECTOR ( 'NONE', #137666, 1000.000000000000000 ) ;
#130542=CARTESIAN_POINT ( 'NONE',  ( -16.87036670365549895, 9.989418819312803066, -146.5204398826979855 ) ) ;
#130639=ORIENTED_EDGE ( 'NONE', *, *, #96111, .F. ) ;
#130674=EDGE_CURVE ( 'NONE', #70072, #83264, #85647, .T. ) ;
#130679=EDGE_CURVE ( 'NONE', #107290, #135886, #242835, .T. ) ;
#130795=CARTESIAN_POINT ( 'NONE',  ( 18.54999999999999716, 8.750000000011182166, -143.2500000000000284 ) ) ;
#131192=EDGE_CURVE ( 'NONE', #67383, #194499, #240416, .T. ) ;
#131289=CARTESIAN_POINT ( 'NONE',  ( -16.93339986808596365, 10.00510392857707487, -146.5659936718128904 ) ) ;
#131387=CARTESIAN_POINT ( 'NONE',  ( -12.93407622233968368, 9.417789466963366607, -149.3573845439769343 ) ) ;
#131453=EDGE_CURVE ( 'NONE', #198318, #43558, #255778, .T. ) ;
#131764=DIRECTION ( 'NONE',  ( 0.5932847527679310229, -0.8049926720990042694, 0.000000000000000000 ) ) ;
#131864=CARTESIAN_POINT ( 'NONE',  ( 21.72449340488910607, 10.28395627750226815, -154.8500000000000227 ) ) ;
#131889=CARTESIAN_POINT ( 'NONE',  ( -16.89146115310545682, 9.951443245667611848, -154.8548224189542566 ) ) ;
#132095=AXIS2_PLACEMENT_3D ( 'NONE', #190447, #92592, #255477 ) ;
#132121=VECTOR ( 'NONE', #205187, 1000.000000000000000 ) ;
#132177=DIRECTION ( 'NONE',  ( -0.000000000000000000, 1.000000000000000000, 0.000000000000000000 ) ) ;
#132294=ADVANCED_FACE ( 'NONE', ( #106232 ), #26744, .F. ) ;
#132346=ADVANCED_BREP_SHAPE_REPRESENTATION ( '', ( #112300, #2425 ), #227291 ) ;
#132557=ORIENTED_EDGE ( 'NONE', *, *, #153047, .T. ) ;
#132717=DIRECTION ( 'NONE',  ( -1.000000000000000000, 0.000000000000000000, 0.000000000000000000 ) ) ;
#132980=CARTESIAN_POINT ( 'NONE',  ( -16.77779411440718249, 9.946101447118758543, -154.8369425829954764 ) ) ;
#133097=ORIENTED_EDGE ( 'NONE', *, *, #210093, .T. ) ;
#133187=CARTESIAN_POINT ( 'NONE',  ( -18.34374000495059676, 11.47316190337362940, -158.2500000000000284 ) ) ;
#133280=VECTOR ( 'NONE', #226082, 1000.000000000000000 ) ;
#133343=AXIS2_PLACEMENT_3D ( 'NONE', #105724, #164455, #143596 ) ;
#133475=B_SPLINE_CURVE_WITH_KNOTS ( 'NONE', 3,
 ( #237986, #161042, #184440, #102300, #222257, #244414, #43660, #81458, #201435, #86604, #142734, #22833, #85317, #124488 ),
 .UNSPECIFIED., .F., .F.,
 ( 4, 2, 2, 2, 2, 2, 4 ),
 ( 0.000000000000000000, 2.389617747646589612E-05, 4.779235495293179223E-05, 9.558470990578389560E-05, 0.0001911694198114880752, 0.0003823388396228947811, 0.0007646776792456254140 ),
 .UNSPECIFIED. ) ;
#133576=DIRECTION ( 'NONE',  ( -1.000000000000000000, -0.000000000000000000, -0.000000000000000000 ) ) ;
#133856=CARTESIAN_POINT ( 'NONE',  ( -16.94037747912386038, 10.01353938249748410, -146.5511309579755164 ) ) ;
#133949=CARTESIAN_POINT ( 'NONE',  ( -14.45443560709635911, 9.450592112144859058, -149.0561883188084096 ) ) ;
#133980=ADVANCED_FACE ( 'NONE', ( #49783 ), #74536, .F. ) ;
#134022=CARTESIAN_POINT ( 'NONE',  ( -16.89021194854739605, 9.950000000011137047, -154.7425681316044006 ) ) ;
#134101=FACE_OUTER_BOUND ( 'NONE', #248213, .T. ) ;
#134179=VERTEX_POINT ( 'NONE', #186440 ) ;
#134313=ORIENTED_EDGE ( 'NONE', *, *, #131453, .T. ) ;
#134477=CARTESIAN_POINT ( 'NONE',  ( -16.93589915522259304, 10.00862525870701347, -154.9405601019603296 ) ) ;
#134616=ORIENTED_EDGE ( 'NONE', *, *, #81305, .T. ) ;
#134707=( BOUNDED_SURFACE ( )  B_SPLINE_SURFACE ( 3, 2, ( 
 ( #251109, #72513, #52925 ),
 ( #172928, #114186, #174210 ),
 ( #220688, #86277, #124165 ),
 ( #45895, #121613, #84986 ),
 ( #164572, #160743, #244086 ),
 ( #42064, #6767, #65451 ),
 ( #44620, #202403, #142421 ),
 ( #201118, #47153, #144977 ),
 ( #143704, #125443, #105842 ),
 ( #224526, #242803, #23799 ) ),
 .UNSPECIFIED., .F., .F., .F. ) 
 B_SPLINE_SURFACE_WITH_KNOTS ( ( 4, 2, 2, 2, 4 ),
 ( 3, 3 ),
 ( 0.002161241639767785133, 0.002579950749617447234, 0.002789305304542278284, 0.002893982582004694243, 0.002998659859467109768 ),
 ( 0.000000000000000000, 1.000000000000000000 ),
 .UNSPECIFIED. ) 
 GEOMETRIC_REPRESENTATION_ITEM ( )  RATIONAL_B_SPLINE_SURFACE ( (
 ( 1.000000000000000000, 0.7071067811864923947, 1.000000000000000000),
 ( 1.000000000000000000, 0.7632447400664384984, 1.000000000000000000),
 ( 1.000000000000000000, 0.8158073005108742448, 1.000000000000000000),
 ( 1.000000000000000000, 0.8906973462396178265, 1.000000000000000000),
 ( 1.000000000000000000, 0.9149408947802152303, 1.000000000000000000),
 ( 1.000000000000000000, 0.9493368785274697297, 1.000000000000000000),
 ( 1.000000000000000000, 0.9605194247157555765, 1.000000000000000000),
 ( 1.000000000000000000, 0.9803630264780319736, 1.000000000000000000),
 ( 1.000000000000000000, 0.9900844824271819444, 1.000000000000000000),
 ( 1.000000000000000000, 0.9894588281429244070, 1.000000000000000000) ) ) 
 REPRESENTATION_ITEM ( '' )  SURFACE ( )  );
#134819=CARTESIAN_POINT ( 'NONE',  ( -18.40000000000000213, 11.75000000001113953, -158.2500000000000284 ) ) ;
#134864=CARTESIAN_POINT ( 'NONE',  ( -16.77308656112214891, 9.950000000011138823, -154.8498068082977284 ) ) ;
#134898=CARTESIAN_POINT ( 'NONE',  ( -18.40000000000000213, 11.75000000001113953, -146.6500000000000341 ) ) ;
#134980=CARTESIAN_POINT ( 'NONE',  ( -16.92209698673685025, 9.950000000011138823, -154.7893644329461722 ) ) ;
#135002=EDGE_CURVE ( 'NONE', #194499, #221938, #175557, .T. ) ;
#135160=DIRECTION ( 'NONE',  ( 0.000000000000000000, 0.000000000000000000, 1.000000000000000000 ) ) ;
#135180=DIRECTION ( 'NONE',  ( 0.7071067811865463515, 0.7071067811865487940, 7.587431340288849180E-16 ) ) ;
#135216=DIRECTION ( 'NONE',  ( 1.000000000000000000, 0.000000000000000000, 0.000000000000000000 ) ) ;
#135222=ORIENTED_EDGE ( 'NONE', *, *, #38740, .F. ) ;
#135223=CARTESIAN_POINT ( 'NONE',  ( -16.89268316805465986, 9.951721813253337601, -154.8557524785455541 ) ) ;
#135226=CARTESIAN_POINT ( 'NONE',  ( -15.70407651835960650, 9.355806591641286474, -150.2911025315461870 ) ) ;
#135886=VERTEX_POINT ( 'NONE', #120626 ) ;
#135947=EDGE_CURVE ( 'NONE', #5552, #168403, #244394, .T. ) ;
#136145=DIRECTION ( 'NONE',  ( -1.073024830501117725E-15, -0.000000000000000000, -1.000000000000000000 ) ) ;
#136161=CARTESIAN_POINT ( 'NONE',  ( -17.78241384944316650, 10.85557575281093357, -144.2490376724881003 ) ) ;
#136299=ORIENTED_EDGE ( 'NONE', *, *, #185059, .T. ) ;
#136679=VERTEX_POINT ( 'NONE', #204293 ) ;
#136774=VECTOR ( 'NONE', #135180, 999.9999999999998863 ) ;
#136844=ADVANCED_FACE ( 'NONE', ( #231584 ), #9959, .F. ) ;
#136865=ADVANCED_FACE ( 'NONE', ( #229018 ), #251114, .T. ) ;
#136872=CIRCLE ( 'NONE', #170244, 14.20833333333333748 ) ;
#137160=CARTESIAN_POINT ( 'NONE',  ( -16.81744102076749314, 9.950000000011142376, -146.6500000000000341 ) ) ;
#137253=EDGE_LOOP ( 'NONE', ( #86344, #245904, #191439, #164732 ) ) ;
#137349=( GEOMETRIC_REPRESENTATION_CONTEXT ( 3 ) GLOBAL_UNCERTAINTY_ASSIGNED_CONTEXT ( ( #92064 ) ) GLOBAL_UNIT_ASSIGNED_CONTEXT ( ( #241416, #223114, #242677 ) ) REPRESENTATION_CONTEXT ( 'NONE', 'WORKASPACE' ) );
#137493=CARTESIAN_POINT ( 'NONE',  ( -16.87683809663752399, 23.65833333334447985, -150.7500000000000284 ) ) ;
#137666=DIRECTION ( 'NONE',  ( -0.000000000000000000, 1.000000000000000000, -0.000000000000000000 ) ) ;
#137906=DIRECTION ( 'NONE',  ( -0.000000000000000000, -0.000000000000000000, 1.000000000000000000 ) ) ;
#138091=VERTEX_POINT ( 'NONE', #119383 ) ;
#138093=ORIENTED_EDGE ( 'NONE', *, *, #26837, .T. ) ;
#138283=EDGE_CURVE ( 'NONE', #198318, #156630, #192206, .T. ) ;
#138444=EDGE_CURVE ( 'NONE', #129669, #221938, #184165, .T. ) ;
#138449=FACE_OUTER_BOUND ( 'NONE', #148231, .T. ) ;
#138597=EDGE_LOOP ( 'NONE', ( #24798, #174207, #79744, #21369, #79818 ) ) ;
#138694=CARTESIAN_POINT ( 'NONE',  ( -16.87683809663752399, 9.850000000011144508, -147.4023640181963515 ) ) ;
#138704=CARTESIAN_POINT ( 'NONE',  ( -16.88705144915419964, 9.950000000011138823, -154.5690214052880265 ) ) ;
#138760=CARTESIAN_POINT ( 'NONE',  ( 18.39999999999998082, 11.47316190337362585, -143.2500000000000284 ) ) ;
#138761=ORIENTED_EDGE ( 'NONE', *, *, #104725, .T. ) ;
#138804=ADVANCED_FACE ( 'NONE', ( #182279 ), #98840, .T. ) ;
#138826=CARTESIAN_POINT ( 'NONE',  ( -12.48127053791145258, 9.376580978055098825, -151.6269462470119720 ) ) ;
#138980=VERTEX_POINT ( 'NONE', #28368 ) ;
#139119=CIRCLE ( 'NONE', #9972, 0.9000000000000014655 ) ;
#139240=DIRECTION ( 'NONE',  ( -3.035766082959430717E-14, 0.000000000000000000, -1.000000000000000000 ) ) ;
#139378=ORIENTED_EDGE ( 'NONE', *, *, #158264, .F. ) ;
#139553=VERTEX_POINT ( 'NONE', #73602 ) ;
#139594=ORIENTED_EDGE ( 'NONE', *, *, #207474, .F. ) ;
#139969=EDGE_CURVE ( 'NONE', #81862, #139553, #74504, .T. ) ;
#140124=CARTESIAN_POINT ( 'NONE',  ( -17.05016517655658603, 9.950000000011137047, -154.8273020040062420 ) ) ;
#140133=CARTESIAN_POINT ( 'NONE',  ( -15.75000000000000355, 9.350000000011140955, -150.7500000000000284 ) ) ;
#140317=AXIS2_PLACEMENT_3D ( 'NONE', #59924, #199484, #20850 ) ;
#140400=DIRECTION ( 'NONE',  ( -1.000000000000000000, 0.000000000000000000, 0.000000000000000000 ) ) ;
#140407=CARTESIAN_POINT ( 'NONE',  ( -16.78569801330232281, 9.947933733124651567, -146.6569129053475251 ) ) ;
#140697=DIRECTION ( 'NONE',  ( -1.020425574104004196E-15, -1.210927747993693964E-31, 1.000000000000000000 ) ) ;
#140773=FACE_OUTER_BOUND ( 'NONE', #199560, .T. ) ;
#140833=CARTESIAN_POINT ( 'NONE',  ( -16.91256925476569961, 9.985731158139330432, -154.9676424890052999 ) ) ;
#140853=DIRECTION ( 'NONE',  ( -0.7071067811865487940, 0.7071067811865463515, 0.000000000000000000 ) ) ;
#141034=DIRECTION ( 'NONE',  ( 1.186688945009009831E-16, -1.000000000000000000, 0.000000000000000000 ) ) ;
#141204=DIRECTION ( 'NONE',  ( -0.000000000000000000, -0.000000000000000000, -1.000000000000000000 ) ) ;
#141246=AXIS2_PLACEMENT_3D ( 'NONE', #144944, #208796, #225761 ) ;
#141420=ORIENTED_EDGE ( 'NONE', *, *, #155134, .F. ) ;
#141433=CARTESIAN_POINT ( 'NONE',  ( -13.54036565897076194, 9.451541661396669625, -152.4538754988305982 ) ) ;
#141547=CYLINDRICAL_SURFACE ( 'NONE', #114644, 0.1999999999999987899 ) ;
#141553=CARTESIAN_POINT ( 'NONE',  ( 18.54999999999999716, 8.750000000011182166, -154.8500000000000227 ) ) ;
#141637=CARTESIAN_POINT ( 'NONE',  ( 12.33938619321248176, 9.360723793997193454, -151.3139271946067481 ) ) ;
#141855=VERTEX_POINT ( 'NONE', #223955 ) ;
#142126=EDGE_CURVE ( 'NONE', #149588, #121114, #159860, .T. ) ;
#142421=CARTESIAN_POINT ( 'NONE',  ( -16.82542659449978117, 9.934499891438612451, -146.7446356000260437 ) ) ;
#142426=ORIENTED_EDGE ( 'NONE', *, *, #4342, .F. ) ;
#142734=CARTESIAN_POINT ( 'NONE',  ( -16.85939591225058720, 9.905226478399001167, -146.9600682464690635 ) ) ;
#142807=ORIENTED_EDGE ( 'NONE', *, *, #77049, .T. ) ;
#142809=AXIS2_PLACEMENT_3D ( 'NONE', #13246, #91488, #111044 ) ;
#142841=PLANE ( 'NONE',  #14688 ) ;
#142896=CARTESIAN_POINT ( 'NONE',  ( 12.26145404764309355, 9.351413679112544841, -150.9803435675490277 ) ) ;
#142959=CARTESIAN_POINT ( 'NONE',  ( -16.77779411503078322, 9.946101446935278645, -146.6630574176198536 ) ) ;
#143250=DIRECTION ( 'NONE',  ( 0.000000000000000000, 0.000000000000000000, 1.000000000000000000 ) ) ;
#143472=CARTESIAN_POINT ( 'NONE',  ( 15.74999999999999645, 9.350000000011139178, -150.7500000000000284 ) ) ;
#143596=DIRECTION ( 'NONE',  ( 0.000000000000000000, -0.000000000000000000, -1.000000000000000000 ) ) ;
#143615=DIRECTION ( 'NONE',  ( -0.000000000000000000, -0.000000000000000000, -1.000000000000000000 ) ) ;
#143704=CARTESIAN_POINT ( 'NONE',  ( -16.80891096016330266, 9.950000000011137047, -146.6323371927319101 ) ) ;
#143706=CIRCLE ( 'NONE', #89526, 1.500000000000001332 ) ;
#143855=LINE ( 'NONE', #172475, #13872 ) ;
#143978=VERTEX_POINT ( 'NONE', #184855 ) ;
#144026=CARTESIAN_POINT ( 'NONE',  ( 18.39999999999999503, 11.47316190337363828, -146.6500000000000341 ) ) ;
#144058=FACE_OUTER_BOUND ( 'NONE', #146029, .T. ) ;
#144182=EDGE_CURVE ( 'NONE', #134179, #136679, #43975, .T. ) ;
#144434=FACE_OUTER_BOUND ( 'NONE', #225006, .T. ) ;
#144536=PLANE ( 'NONE',  #178037 ) ;
#144582=SHAPE_DEFINITION_REPRESENTATION ( #201697, #63487 ) ;
#144826=CARTESIAN_POINT ( 'NONE',  ( -16.87242674293850797, 9.950000000011138823, -146.6489097536276631 ) ) ;
#144859=SURFACE_STYLE_USAGE ( .BOTH. , #84856 ) ;
#144927=EDGE_LOOP ( 'NONE', ( #149999, #203446, #161183, #48233 ) ) ;
#144944=CARTESIAN_POINT ( 'NONE',  ( -21.64999999999999858, 10.05000000001113847, -146.7500000000000284 ) ) ;
#144977=CARTESIAN_POINT ( 'NONE',  ( -16.80621392010912984, 9.942202577518864715, -146.6895919654172076 ) ) ;
#145088=LINE ( 'NONE', #201222, #231546 ) ;
#145205=DIRECTION ( 'NONE',  ( -0.000000000000000000, 0.000000000000000000, -1.000000000000000000 ) ) ;
#145423=LINE ( 'NONE', #245825, #113609 ) ;
#145485=CARTESIAN_POINT ( 'NONE',  ( 15.66039659514495774, 9.360749169926261715, -151.3145701406073158 ) ) ;
#145596=EDGE_CURVE ( 'NONE', #209272, #190690, #86940, .T. ) ;
#145815=CYLINDRICAL_SURFACE ( 'NONE', #191724, 0.09999999999998898659 ) ;
#146029=EDGE_LOOP ( 'NONE', ( #181898, #75122, #59083, #175598, #250880, #180831, #121999, #60839, #180764, #217391, #91269, #134313, #248024, #134616 ) ) ;
#146040=CARTESIAN_POINT ( 'NONE',  ( -18.40000000000000213, 11.33174054713631662, -146.6500000000000341 ) ) ;
#146121=CARTESIAN_POINT ( 'NONE',  ( -16.91049119928364775, 9.950000000011138823, -146.6182796068091818 ) ) ;
#146135=CARTESIAN_POINT ( 'NONE',  ( 20.04999999999999716, 8.750000000011173285, -146.6500000000000341 ) ) ;
#146160=CARTESIAN_POINT ( 'NONE',  ( 14.22821877134046709, 9.456028260519072859, -149.0111980350657745 ) ) ;
#146262=CARTESIAN_POINT ( 'NONE',  ( -16.94165728009537375, 9.987869755934932314, -154.8910550085101931 ) ) ;
#146483=FACE_OUTER_BOUND ( 'NONE', #67487, .T. ) ;
#146742=CARTESIAN_POINT ( 'NONE',  ( 15.07585980824112148, 9.417632963117448242, -152.1489484657322748 ) ) ;
#146751=CARTESIAN_POINT ( 'NONE',  ( 17.23472005113826810, 10.30788195451192202, -156.0465768600687113 ) ) ;
#146756=VECTOR ( 'NONE', #177210, 1000.000000000000000 ) ;
#146772=ORIENTED_EDGE ( 'NONE', *, *, #131192, .F. ) ;
#146967=ORIENTED_EDGE ( 'NONE', *, *, #54871, .F. ) ;
#147007=VECTOR ( 'NONE', #233209, 1000.000000000000000 ) ;
#147067=DIRECTION ( 'NONE',  ( 1.000000000000000000, -0.000000000000000000, -0.000000000000000000 ) ) ;
#147160=DIRECTION ( 'NONE',  ( -0.000000000000000000, -0.000000000000000000, -1.000000000000000000 ) ) ;
#147197=CARTESIAN_POINT ( 'NONE',  ( 15.48841904831874849, 8.561580951692381092, -146.6500000000000341 ) ) ;
#147256=EDGE_CURVE ( 'NONE', #138091, #135886, #56530, .T. ) ;
#147455=ORIENTED_EDGE ( 'NONE', *, *, #144182, .F. ) ;
#147913=AXIS2_PLACEMENT_3D ( 'NONE', #151609, #35525, #231141 ) ;
#147936=ORIENTED_EDGE ( 'NONE', *, *, #84462, .T. ) ;
#148046=FACE_OUTER_BOUND ( 'NONE', #37012, .T. ) ;
#148162=CARTESIAN_POINT ( 'NONE',  ( -16.94107738177414291, 10.01423928514777373, -154.9500000000000455 ) ) ;
#148196=LINE ( 'NONE', #212042, #8540 ) ;
#148231=EDGE_LOOP ( 'NONE', ( #249271, #43967, #94522, #130639, #147455 ) ) ;
#148406=DIRECTION ( 'NONE',  ( -1.000000000000000000, 0.000000000000000000, 0.000000000000000000 ) ) ;
#148532=CARTESIAN_POINT ( 'NONE',  ( -18.34374000495060386, 11.47316190337362585, -143.2500000000000284 ) ) ;
#148686=EDGE_CURVE ( 'NONE', #49221, #143978, #117146, .T. ) ;
#148726=DIRECTION ( 'NONE',  ( -1.073024830501117725E-15, -0.000000000000000000, -1.000000000000000000 ) ) ;
#148986=ORIENTED_EDGE ( 'NONE', *, *, #177993, .F. ) ;
#149005=VECTOR ( 'NONE', #25398, 1000.000000000000000 ) ;
#149085=B_SPLINE_CURVE_WITH_KNOTS ( 'NONE', 3,
 ( #250587, #116242, #134477, #254421, #34156, #13280, #233615, #214043, #32877, #96623, #191943, #193208, #75814, #172395, #57512, #210204 ),
 .UNSPECIFIED., .F., .F.,
 ( 4, 3, 3, 3, 3, 4 ),
 ( 0.000000000000000000, 1.810570668010836920E-05, 2.740575833572790496E-05, 4.256816319437009604E-05, 5.213463471025706227E-05, 6.641585710719227482E-05 ),
 .UNSPECIFIED. ) ;
#149479=CARTESIAN_POINT ( 'NONE',  ( -18.40000000000000213, 11.47316190337364183, -154.8914213562373448 ) ) ;
#149588=VERTEX_POINT ( 'NONE', #87674 ) ;
#149630=ORIENTED_EDGE ( 'NONE', *, *, #213404, .T. ) ;
#149679=ORIENTED_EDGE ( 'NONE', *, *, #131453, .F. ) ;
#149728=TOROIDAL_SURFACE ( 'NONE', #78751, 14.20833333333334103, 0.1000000000000000056 ) ;
#149743=AXIS2_PLACEMENT_3D ( 'NONE', #182138, #3479, #244659 ) ;
#149783=DIRECTION ( 'NONE',  ( -1.646408749285562691E-14, 1.000000000000000000, 0.000000000000000000 ) ) ;
#149818=LINE ( 'NONE', #228056, #57951 ) ;
#149829=CARTESIAN_POINT ( 'NONE',  ( -18.34804628011471195, 11.47316190337353525, -143.2500000000000284 ) ) ;
#149985=CARTESIAN_POINT ( 'NONE',  ( -16.77828822459933633, 9.946229375067616729, -154.8373717490810861 ) ) ;
#149992=EDGE_CURVE ( 'NONE', #139553, #221299, #219434, .T. ) ;
#149999=ORIENTED_EDGE ( 'NONE', *, *, #84262, .T. ) ;
#150147=EDGE_CURVE ( 'NONE', #9223, #11705, #119698, .T. ) ;
#150201=CIRCLE ( 'NONE', #129333, 1.749999999999998002 ) ;
#150300=CARTESIAN_POINT ( 'NONE',  ( -16.87683809663752399, 9.850000000011144508, -154.0976359818037054 ) ) ;
#150374=ORIENTED_EDGE ( 'NONE', *, *, #193849, .F. ) ;
#150472=CARTESIAN_POINT ( 'NONE',  ( -18.40000000000000213, 8.822561741677553471, -158.2500000000000284 ) ) ;
#150498=EDGE_CURVE ( 'NONE', #203266, #180463, #218225, .T. ) ;
#150571=DIRECTION ( 'NONE',  ( -1.000000000000000000, 1.652117596168391700E-15, 0.000000000000000000 ) ) ;
#150631=B_SPLINE_CURVE_WITH_KNOTS ( 'NONE', 3,
 ( #179570, #118302, #19192, #120891, #183409, #140407, #58295, #23069, #99977, #201673, #142959, #202955, #79144 ),
 .UNSPECIFIED., .F., .F.,
 ( 4, 3, 3, 3, 4 ),
 ( 1.110764993427085326E-16, 1.946463881814652902E-05, 3.922356109943681788E-05, 4.215060953237600338E-05, 4.415117091092905685E-05 ),
 .UNSPECIFIED. ) ;
#150791=DIRECTION ( 'NONE',  ( 1.073024830501117725E-15, 0.000000000000000000, 1.000000000000000000 ) ) ;
#150854=CARTESIAN_POINT ( 'NONE',  ( -16.93658211146646408, 9.994108662352344297, -146.5957049300443487 ) ) ;
#151128=CARTESIAN_POINT ( 'NONE',  ( -16.77683809663752257, 23.65833333334447985, -150.7500000000000284 ) ) ;
#151298=VERTEX_POINT ( 'NONE', #76936 ) ;
#151299=CARTESIAN_POINT ( 'NONE',  ( 18.39999999999999503, 11.75000000001113953, -158.2500000000000284 ) ) ;
#151525=ORIENTED_EDGE ( 'NONE', *, *, #130679, .T. ) ;
#151556=FACE_OUTER_BOUND ( 'NONE', #60840, .T. ) ;
#151609=CARTESIAN_POINT ( 'NONE',  ( 20.99999999999999645, 9.750000000011137757, -143.2500000000000284 ) ) ;
#151802=ORIENTED_EDGE ( 'NONE', *, *, #8624, .T. ) ;
#151958=DIRECTION ( 'NONE',  ( 1.000000000000000000, 0.000000000000000000, 0.000000000000000000 ) ) ;
#151968=CIRCLE ( 'NONE', #5594, 1.749999999999999778 ) ;
#152200=( BOUNDED_CURVE ( )  B_SPLINE_CURVE ( 3, ( #6664, #165772, #187894, #50904 ),
 .UNSPECIFIED., .F., .F. ) 
 B_SPLINE_CURVE_WITH_KNOTS ( ( 4, 4 ),
 ( 5.731445031868799056, 5.983100554402348337 ),
 .UNSPECIFIED. ) 
 CURVE ( )  GEOMETRIC_REPRESENTATION_ITEM ( )  RATIONAL_B_SPLINE_CURVE ( ( 1.000000000000000000, 0.9947294176030464508, 0.9947294176030464508, 1.000000000000000000 ) ) 
 REPRESENTATION_ITEM ( '' )  );
#152381=EDGE_CURVE ( 'NONE', #199264, #55215, #34046, .T. ) ;
#152718=FACE_OUTER_BOUND ( 'NONE', #215790, .T. ) ;
#153047=EDGE_CURVE ( 'NONE', #166383, #103596, #148196, .T. ) ;
#153209=CARTESIAN_POINT ( 'NONE',  ( -16.85722902420155123, 9.950000000011138823, -154.7344525262302284 ) ) ;
#153211=CARTESIAN_POINT ( 'NONE',  ( 20.73486653747088937, 7.750000000011182166, -146.6500000000000341 ) ) ;
#153330=CARTESIAN_POINT ( 'NONE',  ( -16.87242674293849731, 9.950000000011138823, -154.8510902463723937 ) ) ;
#153476=CARTESIAN_POINT ( 'NONE',  ( -16.93226657140833069, 9.999543822735571297, -146.5787131109736379 ) ) ;
#153513=CARTESIAN_POINT ( 'NONE',  ( 0.000000000000000000, 0.000000000000000000, 0.000000000000000000 ) ) ;
#153568=DIRECTION ( 'NONE',  ( 1.186688945009009831E-16, -1.000000000000000000, 0.000000000000000000 ) ) ;
#153577=CARTESIAN_POINT ( 'NONE',  ( -12.84409460144753901, 9.410682294279110849, -149.4311434419483362 ) ) ;
#153657=CARTESIAN_POINT ( 'NONE',  ( -16.97683809663754673, 9.950000000011137047, -154.2284708321106166 ) ) ;
#153707=CARTESIAN_POINT ( 'NONE',  ( -20.65000000000000568, 5.650000000011139001, -143.2500000000000284 ) ) ;
#153760=CARTESIAN_POINT ( 'NONE',  ( -16.97683809663752186, 9.850000000011137402, -147.4023640181965220 ) ) ;
#154243=CARTESIAN_POINT ( 'NONE',  ( -16.86578989773640913, 9.984809801269951990, -154.9646648866222449 ) ) ;
#154495=CARTESIAN_POINT ( 'NONE',  ( -16.84981964351507600, 9.917318234109812281, -154.6303983859796460 ) ) ;
#154546=ORIENTED_EDGE ( 'NONE', *, *, #23437, .F. ) ;
#154614=CARTESIAN_POINT ( 'NONE',  ( -12.60829076262180948, 9.389529397477893724, -151.8171079128937606 ) ) ;
#154700=EDGE_LOOP ( 'NONE', ( #227377, #183611, #149679, #187491, #99490, #209917, #77661, #61968, #175348, #89185, #139378, #142426 ) ) ;
#154724=ORIENTED_EDGE ( 'NONE', *, *, #38740, .T. ) ;
#154813=ORIENTED_EDGE ( 'NONE', *, *, #130679, .F. ) ;
#154952=PRODUCT_DEFINITION_CONTEXT ( 'detailed design', #202408, 'design' ) ;
#155118=EDGE_CURVE ( 'NONE', #156798, #127092, #87962, .T. ) ;
#155131=CARTESIAN_POINT ( 'NONE',  ( -17.29158576265544056, 10.36474766602906783, -145.4172417552078400 ) ) ;
#155134=EDGE_CURVE ( 'NONE', #166775, #39025, #40706, .T. ) ;
#155142=ORIENTED_EDGE ( 'NONE', *, *, #120706, .T. ) ;
#155194=EDGE_CURVE ( 'NONE', #221934, #143978, #98098, .T. ) ;
#155383=ADVANCED_FACE ( 'NONE', ( #243989 ), #28857, .F. ) ;
#155398=ORIENTED_EDGE ( 'NONE', *, *, #8624, .F. ) ;
#155670=LINE ( 'NONE', #73562, #68103 ) ;
#155896=CARTESIAN_POINT ( 'NONE',  ( -12.42749937872396515, 9.370689921613767126, -151.5264651266610656 ) ) ;
#156074=DIRECTION ( 'NONE',  ( 1.000000000000000000, 0.000000000000000000, 0.000000000000000000 ) ) ;
#156291=VECTOR ( 'NONE', #161099, 1000.000000000000000 ) ;
#156362=LINE ( 'NONE', #235851, #74463 ) ;
#156536=DIRECTION ( 'NONE',  ( -0.5932847527679310229, 0.8049926720990042694, -6.366092712777067056E-16 ) ) ;
#156630=VERTEX_POINT ( 'NONE', #37858 ) ;
#156643=ORIENTED_EDGE ( 'NONE', *, *, #28276, .F. ) ;
#156647=EDGE_CURVE ( 'NONE', #225791, #254838, #250456, .T. ) ;
#156677=AXIS2_PLACEMENT_3D ( 'NONE', #103528, #183101, #4436 ) ;
#156798=VERTEX_POINT ( 'NONE', #241185 ) ;
#157042=CARTESIAN_POINT ( 'NONE',  ( -16.77180007708461318, 9.950000000011137047, -154.8643858810451945 ) ) ;
#157294=CARTESIAN_POINT ( 'NONE',  ( 23.04999999999999716, 8.822561741677553471, -143.2500000000000284 ) ) ;
#157308=VECTOR ( 'NONE', #133576, 1000.000000000000000 ) ;
#157401=VERTEX_POINT ( 'NONE', #210713 ) ;
#158042=EDGE_CURVE ( 'NONE', #159239, #49118, #143706, .T. ) ;
#158099=ORIENTED_EDGE ( 'NONE', *, *, #24217, .F. ) ;
#158216=CARTESIAN_POINT ( 'NONE',  ( 16.87683809663750267, 9.950000000011138823, -146.6500000000000341 ) ) ;
#158264=EDGE_CURVE ( 'NONE', #236861, #129669, #79631, .T. ) ;
#158312=CARTESIAN_POINT ( 'NONE',  ( -20.65000000000000568, 5.650000000011139001, -146.6500000000000341 ) ) ;
#158385=CARTESIAN_POINT ( 'NONE',  ( 18.39999999999999503, 11.75000000001113953, -146.6500000000000341 ) ) ;
#158448=CARTESIAN_POINT ( 'NONE',  ( -18.40000000000000213, 5.650000000011139001, -146.6500000000000341 ) ) ;
#158578=DIRECTION ( 'NONE',  ( -1.000000000000000000, 0.000000000000000000, 0.000000000000000000 ) ) ;
#159082=CARTESIAN_POINT ( 'NONE',  ( -16.86578989773641979, 9.984809801269951990, -146.5353351133777835 ) ) ;
#159188=EDGE_CURVE ( 'NONE', #151298, #141855, #108047, .T. ) ;
#159201=EDGE_LOOP ( 'NONE', ( #186380, #53663, #58383, #133097 ) ) ;
#159216=CARTESIAN_POINT ( 'NONE',  ( -18.40000000000000213, 11.75000000001113953, -146.6500000000000341 ) ) ;
#159239=VERTEX_POINT ( 'NONE', #176567 ) ;
#159348=CARTESIAN_POINT ( 'NONE',  ( -18.41431012584569515, 11.48747202921932775, -158.2732360131017231 ) ) ;
#159841=DIRECTION ( 'NONE',  ( 1.000000000000000000, 1.186688945009010077E-16, 0.000000000000000000 ) ) ;
#159860=LINE ( 'NONE', #141553, #190149 ) ;
#160286=ORIENTED_EDGE ( 'NONE', *, *, #46324, .T. ) ;
#160296=DIRECTION ( 'NONE',  ( -0.7071067811865487940, 0.7071067811865463515, -7.215498431451184074E-16 ) ) ;
#160318=ADVANCED_FACE ( 'NONE', ( #148046 ), #168238, .F. ) ;
#160366=CARTESIAN_POINT ( 'NONE',  ( -15.75000000000000355, 9.850000000011133849, -150.7500000000000284 ) ) ;
#160426=CARTESIAN_POINT ( 'NONE',  ( -16.85718274719485876, 9.976142314632889807, -154.9366536678175237 ) ) ;
#160518=ORIENTED_EDGE ( 'NONE', *, *, #150498, .F. ) ;
#160576=ORIENTED_EDGE ( 'NONE', *, *, #103498, .T. ) ;
#160619=CARTESIAN_POINT ( 'NONE',  ( -16.87036670365549540, 9.989418819312804843, -146.5204398826979855 ) ) ;
#160743=CARTESIAN_POINT ( 'NONE',  ( -16.87998658237741978, 9.950000000011138823, -146.8636395677385167 ) ) ;
#161042=CARTESIAN_POINT ( 'NONE',  ( -16.78493832629886739, 9.945835743215301505, -146.6639490191042228 ) ) ;
#161099=DIRECTION ( 'NONE',  ( 1.186688945009010077E-16, -1.000000000000000000, -0.000000000000000000 ) ) ;
#161145=CARTESIAN_POINT ( 'NONE',  ( -23.25000000000000355, 11.75000000001113953, -146.6500000000000341 ) ) ;
#161183=ORIENTED_EDGE ( 'NONE', *, *, #211440, .F. ) ;
#161217=ORIENTED_EDGE ( 'NONE', *, *, #135947, .F. ) ;
#161250=EDGE_CURVE ( 'NONE', #194499, #7029, #9857, .T. ) ;
#161353=ORIENTED_EDGE ( 'NONE', *, *, #82560, .T. ) ;
#161539=B_SPLINE_CURVE_WITH_KNOTS ( 'NONE', 3,
 ( #29890, #207231, #28633, #229359, #7741, #149829, #148532 ),
 .UNSPECIFIED., .F., .F.,
 ( 4, 3, 4 ),
 ( 0.000000000000000000, 4.520325912680675723E-05, 5.794988040901448781E-05 ),
 .UNSPECIFIED. ) ;
#161699=CARTESIAN_POINT ( 'NONE',  ( -16.86445178670583900, 9.962211629127157408, -154.8907774381173681 ) ) ;
#161754=CIRCLE ( 'NONE', #32774, 0.9000000000000014655 ) ;
#161894=VECTOR ( 'NONE', #35774, 1000.000000000000000 ) ;
#161897=CARTESIAN_POINT ( 'NONE',  ( -18.44085059012131822, 11.51401249349495437, -143.2596946808784821 ) ) ;
#161910=CARTESIAN_POINT ( 'NONE',  ( 13.76927104934457802, 9.455987233623899257, -149.0115311668978677 ) ) ;
#161918=CARTESIAN_POINT ( 'NONE',  ( -16.94445028196808778, 9.992063609708889516, -146.6073301784184935 ) ) ;
#161919=CARTESIAN_POINT ( 'NONE',  ( -16.91256925476569961, 9.985731158139333985, -154.9676424890052999 ) ) ;
#162024=EDGE_CURVE ( 'NONE', #221, #166775, #161754, .T. ) ;
#162152=VECTOR ( 'NONE', #147067, 1000.000000000000000 ) ;
#162165=PRODUCT ( 'Snap Open Cable Crossbars 5', 'Snap Open Cable Crossbars 5', '', ( #203292 ) ) ;
#162304=CARTESIAN_POINT ( 'NONE',  ( -14.45422546970483779, 9.450602096099679272, -152.4438959630966792 ) ) ;
#162397=EDGE_CURVE ( 'NONE', #168403, #225332, #187060, .T. ) ;
#162447=CARTESIAN_POINT ( 'NONE',  ( -18.40000000000000213, 11.47867410001105526, -158.2253067836594198 ) ) ;
#162509=CARTESIAN_POINT ( 'NONE',  ( 13.22461703343584638, 9.436662931810237964, -152.3230367322948950 ) ) ;
#162552=ORIENTED_EDGE ( 'NONE', *, *, #240429, .F. ) ;
#162721=CARTESIAN_POINT ( 'NONE',  ( -16.94445028196808778, 9.992063609708889516, -146.6073301784184935 ) ) ;
#162764=DIRECTION ( 'NONE',  ( 1.000000000000000000, 0.000000000000000000, 0.000000000000000000 ) ) ;
#162895=VECTOR ( 'NONE', #60020, 1000.000000000000000 ) ;
#163246=DIRECTION ( 'NONE',  ( -0.7071067811865456854, 0.7071067811865493491, 0.000000000000000000 ) ) ;
#163326=ORIENTED_EDGE ( 'NONE', *, *, #53994, .F. ) ;
#163565=EDGE_CURVE ( 'NONE', #1366, #171058, #133475, .T. ) ;
#163629=B_SPLINE_CURVE_WITH_KNOTS ( 'NONE', 3,
 ( #69363, #249279, #188018, #211425, #126750, #107176, #112338, #131889, #186743, #9357 ),
 .UNSPECIFIED., .F., .F.,
 ( 4, 3, 3, 4 ),
 ( 0.000000000000000000, 1.004626015991471073E-05, 1.831183478184062558E-05, 2.062343583996205056E-05 ),
 .UNSPECIFIED. ) ;
#163893=DIRECTION ( 'NONE',  ( 1.186688945009009831E-16, -1.000000000000000000, 0.000000000000000000 ) ) ;
#164010=CARTESIAN_POINT ( 'NONE',  ( -16.94445028196808778, 9.992063609708889516, -146.6073301784184935 ) ) ;
#164455=DIRECTION ( 'NONE',  ( 0.000000000000000000, -1.000000000000000000, 0.000000000000000000 ) ) ;
#164460=CARTESIAN_POINT ( 'NONE',  ( 15.74999999999999645, 9.350000000011139178, -150.7500000000000284 ) ) ;
#164552=DIRECTION ( 'NONE',  ( 0.000000000000000000, 0.000000000000000000, 1.000000000000000000 ) ) ;
#164562=CARTESIAN_POINT ( 'NONE',  ( -16.27683809663750480, 9.350000000011133849, -143.2500000000000284 ) ) ;
#164572=CARTESIAN_POINT ( 'NONE',  ( -16.92280123533699054, 9.950000000011137047, -146.8506323140851180 ) ) ;
#164732=ORIENTED_EDGE ( 'NONE', *, *, #142126, .T. ) ;
#164746=ORIENTED_EDGE ( 'NONE', *, *, #23437, .T. ) ;
#165136=PLANE ( 'NONE',  #149743 ) ;
#165273=EDGE_CURVE ( 'NONE', #23667, #56249, #231056, .T. ) ;
#165358=ORIENTED_EDGE ( 'NONE', *, *, #53608, .T. ) ;
#165463=EDGE_CURVE ( 'NONE', #226856, #138091, #111834, .T. ) ;
#165714=CARTESIAN_POINT ( 'NONE',  ( -17.11825945287482753, 10.05000000001113847, -146.6500000000000341 ) ) ;
#165772=CARTESIAN_POINT ( 'NONE',  ( -17.71734398241073905, 10.84235722847571814, -144.2748617469944463 ) ) ;
#165823=CARTESIAN_POINT ( 'NONE',  ( -15.55912972643740488, 8.490870273573721150, -154.9500000000000455 ) ) ;
#166068=VECTOR ( 'NONE', #137906, 1000.000000000000000 ) ;
#166383=VERTEX_POINT ( 'NONE', #251913 ) ;
#166486=ORIENTED_EDGE ( 'NONE', *, *, #150147, .F. ) ;
#166581=DIRECTION ( 'NONE',  ( 0.000000000000000000, 0.000000000000000000, -1.000000000000000000 ) ) ;
#166775=VERTEX_POINT ( 'NONE', #31324 ) ;
#167165=ORIENTED_EDGE ( 'NONE', *, *, #35478, .F. ) ;
#167322=VECTOR ( 'NONE', #74652, 1000.000000000000000 ) ;
#167421=LINE ( 'NONE', #171304, #172563 ) ;
#167444=CARTESIAN_POINT ( 'NONE',  ( -20.65000000000000568, 7.250000000011138646, -154.8500000000000227 ) ) ;
#167543=DIRECTION ( 'NONE',  ( -1.000000000000000000, 0.000000000000000000, 0.000000000000000000 ) ) ;
#167545=FACE_OUTER_BOUND ( 'NONE', #231202, .T. ) ;
#167692=CIRCLE ( 'NONE', #109202, 0.9000000000000014655 ) ;
#167976=ORIENTED_EDGE ( 'NONE', *, *, #130674, .F. ) ;
#168153=ORIENTED_EDGE ( 'NONE', *, *, #158042, .T. ) ;
#168238=( BOUNDED_SURFACE ( )  B_SPLINE_SURFACE ( 3, 2, ( 
 ( #108905, #188446, #89331 ),
 ( #37107, #119192, #16261 ),
 ( #253543, #98293, #74951 ),
 ( #175335, #138704, #236549 ),
 ( #154495, #232731, #235266 ),
 ( #57904, #153209, #114033 ),
 ( #78753, #197426, #54066 ),
 ( #254787, #174066, #214419 ),
 ( #233985, #116615, #196149 ),
 ( #194889, #134864, #157042 ) ),
 .UNSPECIFIED., .F., .F., .F. ) 
 B_SPLINE_SURFACE_WITH_KNOTS ( ( 4, 2, 2, 2, 4 ),
 ( 3, 3 ),
 ( 0.002161241639767248670, 0.002579950749615825267, 0.002789305304540113349, 0.002893982582002257390, 0.002998659859464401431 ),
 ( 0.000000000000000000, 1.000000000000000000 ),
 .UNSPECIFIED. ) 
 GEOMETRIC_REPRESENTATION_ITEM ( )  RATIONAL_B_SPLINE_SURFACE ( (
 ( 1.000000000000000000, 0.7071067811865536790, 1.000000000000000000),
 ( 1.000000000000000000, 0.7632447400664924553, 1.000000000000000000),
 ( 1.000000000000000000, 0.8158073005109215403, 1.000000000000000000),
 ( 1.000000000000000000, 0.8906973462396327035, 1.000000000000000000),
 ( 1.000000000000000000, 0.9149408947798607361, 1.000000000000000000),
 ( 1.000000000000000000, 0.9493368785276657951, 1.000000000000000000),
 ( 1.000000000000000000, 0.9605194247158186371, 1.000000000000000000),
 ( 1.000000000000000000, 0.9803630264779832348, 1.000000000000000000),
 ( 1.000000000000000000, 0.9900844824272205802, 1.000000000000000000),
 ( 1.000000000000000000, 0.9894588281429248511, 1.000000000000000000) ) ) 
 REPRESENTATION_ITEM ( '' )  SURFACE ( )  );
#168385=ORIENTED_EDGE ( 'NONE', *, *, #222848, .T. ) ;
#168403=VERTEX_POINT ( 'NONE', #174435 ) ;
#168591=CARTESIAN_POINT ( 'NONE',  ( -17.01825945287481545, 9.950000000011138823, -154.7500000000000284 ) ) ;
#168716=VERTEX_POINT ( 'NONE', #3428 ) ;
#168816=ORIENTED_EDGE ( 'NONE', *, *, #189760, .F. ) ;
#168886=DIRECTION ( 'NONE',  ( -0.000000000000000000, 1.000000000000000000, -0.000000000000000000 ) ) ;
#169138=CARTESIAN_POINT ( 'NONE',  ( -20.65000000000000568, 7.250000000011138646, -143.2500000000000284 ) ) ;
#169169=CARTESIAN_POINT ( 'NONE',  ( -16.93255653858138388, 9.998451453988312920, -146.5816433679896988 ) ) ;
#169326=DIRECTION ( 'NONE',  ( 0.5932847527679310229, -0.8049926720990042694, -6.366092712777067056E-16 ) ) ;
#169341=LINE ( 'NONE', #190159, #26374 ) ;
#169679=ORIENTED_EDGE ( 'NONE', *, *, #245669, .F. ) ;
#169873=LINE ( 'NONE', #8194, #128731 ) ;
#170058=DIRECTION ( 'NONE',  ( -0.000000000000000000, -0.000000000000000000, -1.000000000000000000 ) ) ;
#170191=VECTOR ( 'NONE', #233380, 1000.000000000000000 ) ;
#170197=EDGE_CURVE ( 'NONE', #11705, #71313, #12056, .T. ) ;
#170244=AXIS2_PLACEMENT_3D ( 'NONE', #137493, #20150, #113473 ) ;
#170270=DIRECTION ( 'NONE',  ( 1.000000000000000000, -0.000000000000000000, -0.000000000000000000 ) ) ;
#170404=LINE ( 'NONE', #107803, #256999 ) ;
#170868=CARTESIAN_POINT ( 'NONE',  ( 12.25000000000000000, 9.850000000011137402, -150.7500000000000284 ) ) ;
#170993=EDGE_CURVE ( 'NONE', #209272, #242248, #213136, .T. ) ;
#171058=VERTEX_POINT ( 'NONE', #138694 ) ;
#171191=CYLINDRICAL_SURFACE ( 'NONE', #147913, 0.9000000000000014655 ) ;
#171304=CARTESIAN_POINT ( 'NONE',  ( -18.40000000000000213, 5.650000000011139001, -146.6500000000000341 ) ) ;
#171355=ORIENTED_EDGE ( 'NONE', *, *, #245388, .T. ) ;
#171453=CARTESIAN_POINT ( 'NONE',  ( -16.94445028196807002, 9.992063609708893068, -154.8926698215815634 ) ) ;
#171927=CARTESIAN_POINT ( 'NONE',  ( -16.77683809663752257, 23.65833333334447985, -150.7500000000000284 ) ) ;
#172134=CARTESIAN_POINT ( 'NONE',  ( -17.78043020864320667, 10.85359211201683927, -144.3369508342798042 ) ) ;
#172295=CARTESIAN_POINT ( 'NONE',  ( -16.89797118371580353, 9.976380722655672884, -146.5627066324414045 ) ) ;
#172395=CARTESIAN_POINT ( 'NONE',  ( -16.93860193097148326, 9.993107767340401182, -154.9001383673068801 ) ) ;
#172475=CARTESIAN_POINT ( 'NONE',  ( -33.72168855820451938, 9.950000000011156587, -146.6499999999999773 ) ) ;
#172563=VECTOR ( 'NONE', #30470, 1000.000000000000000 ) ;
#172837=CARTESIAN_POINT ( 'NONE',  ( -18.40000000000000213, 5.650000000011139001, -154.8500000000000227 ) ) ;
#172928=CARTESIAN_POINT ( 'NONE',  ( -16.97683810757273193, 9.950000000011137047, -147.2635767124612869 ) ) ;
#173036=CARTESIAN_POINT ( 'NONE',  ( -16.93583594267724379, 10.00862343506335961, -146.5593908393207982 ) ) ;
#173140=ORIENTED_EDGE ( 'NONE', *, *, #235401, .T. ) ;
#173141=CARTESIAN_POINT ( 'NONE',  ( -12.47155713865591764, 9.375669526436929857, -149.8677900093859705 ) ) ;
#173184=CARTESIAN_POINT ( 'NONE',  ( -23.25000000000000355, 10.05000000001113847, -146.7500000000000284 ) ) ;
#173443=EDGE_CURVE ( 'NONE', #56540, #184760, #7252, .T. ) ;
#173607=ADVANCED_FACE ( 'NONE', ( #17519 ), #235197, .T. ) ;
#173641=ORIENTED_EDGE ( 'NONE', *, *, #89401, .F. ) ;
#173813=EDGE_LOOP ( 'NONE', ( #141420, #155142, #114341, #229239 ) ) ;
#173838=AXIS2_PLACEMENT_3D ( 'NONE', #174444, #71463, #231813 ) ;
#173873=ADVANCED_FACE ( 'NONE', ( #16933, #191741, #91334 ), #113451, .T. ) ;
#174066=CARTESIAN_POINT ( 'NONE',  ( -16.82055514392377304, 9.950000000011137047, -154.8232019254577949 ) ) ;
#174207=ORIENTED_EDGE ( 'NONE', *, *, #207474, .T. ) ;
#174210=CARTESIAN_POINT ( 'NONE',  ( -16.87683809663752754, 9.865889849342865503, -147.2674268070695689 ) ) ;
#174415=DIRECTION ( 'NONE',  ( 1.073024830501117725E-15, -0.000000000000000000, -1.000000000000000000 ) ) ;
#174416=CARTESIAN_POINT ( 'NONE',  ( 13.99999999999999822, 9.850000000011137402, -150.7500000000000284 ) ) ;
#174435=CARTESIAN_POINT ( 'NONE',  ( -21.65000000000000213, 9.950000000011140600, -146.7500000000000284 ) ) ;
#174444=CARTESIAN_POINT ( 'NONE',  ( -23.25000000000000355, 11.75000000001113953, -143.2500000000000284 ) ) ;
#174520=CARTESIAN_POINT ( 'NONE',  ( 12.25000000000000000, 9.850000000011137402, -150.7500000000000284 ) ) ;
#174615=CARTESIAN_POINT ( 'NONE',  ( -16.77683809663752257, 9.945835743215301505, -146.6639490191042228 ) ) ;
#174712=DIRECTION ( 'NONE',  ( -1.000000000000000000, 0.000000000000000000, 0.000000000000000000 ) ) ;
#174843=MECHANICAL_DESIGN_GEOMETRIC_PRESENTATION_REPRESENTATION('',(#87290),#137349);
#175194=CARTESIAN_POINT ( 'NONE',  ( -33.72168855820451938, 9.950000000011156587, -154.8500000000000796 ) ) ;
#175335=CARTESIAN_POINT ( 'NONE',  ( -16.85697194749122829, 9.908543714134735225, -154.5649957323862225 ) ) ;
#175348=ORIENTED_EDGE ( 'NONE', *, *, #111619, .F. ) ;
#175557=LINE ( 'NONE', #193822, #130339 ) ;
#175559=FACE_OUTER_BOUND ( 'NONE', #75984, .T. ) ;
#175598=ORIENTED_EDGE ( 'NONE', *, *, #54344, .F. ) ;
#175670=CARTESIAN_POINT ( 'NONE',  ( -13.54795643572457919, 9.450668889178686527, -149.0555464902073481 ) ) ;
#175737=DIRECTION ( 'NONE',  ( -1.652117596168391700E-15, -1.000000000000000000, 0.000000000000000000 ) ) ;
#175806=EDGE_CURVE ( 'NONE', #226856, #236861, #1885, .T. ) ;
#175974=VECTOR ( 'NONE', #169326, 1000.000000000000000 ) ;
#176040=DIRECTION ( 'NONE',  ( -1.000000000000000000, 0.000000000000000000, 0.000000000000000000 ) ) ;
#176218=FACE_OUTER_BOUND ( 'NONE', #81350, .T. ) ;
#176278=EDGE_CURVE ( 'NONE', #166383, #81086, #253978, .T. ) ;
#176525=CARTESIAN_POINT ( 'NONE',  ( -16.87331047859651179, 9.950000000011142376, -146.6500000000000341 ) ) ;
#176567=CARTESIAN_POINT ( 'NONE',  ( 20.05000000000002913, 7.250000000011171508, -146.6500000000000341 ) ) ;
#176666=CARTESIAN_POINT ( 'NONE',  ( 17.74533788810830259, 10.81849979148194940, -144.3136226749475952 ) ) ;
#176990=CARTESIAN_POINT ( 'NONE',  ( -18.40000000000000213, 11.47316190337364183, -158.2500000000000284 ) ) ;
#177098=FACE_OUTER_BOUND ( 'NONE', #113630, .T. ) ;
#177210=DIRECTION ( 'NONE',  ( -0.000000000000000000, 1.000000000000000000, -0.000000000000000000 ) ) ;
#177271=EDGE_CURVE ( 'NONE', #31535, #203363, #2547, .T. ) ;
#177410=AXIS2_PLACEMENT_3D ( 'NONE', #129394, #128116, #13304 ) ;
#177441=PLANE ( 'NONE',  #103871 ) ;
#177641=EDGE_CURVE ( 'NONE', #121114, #81429, #65702, .T. ) ;
#177897=VECTOR ( 'NONE', #98658, 1000.000000000000000 ) ;
#177993=EDGE_CURVE ( 'NONE', #43053, #81086, #14570, .T. ) ;
#178037=AXIS2_PLACEMENT_3D ( 'NONE', #41627, #160296, #140697 ) ;
#178304=CARTESIAN_POINT ( 'NONE',  ( -21.64999999999999858, 9.350000000011133849, -146.6500000000000341 ) ) ;
#178770=CARTESIAN_POINT ( 'NONE',  ( -18.40000000000000213, 11.33174054713631662, -146.6500000000000341 ) ) ;
#178812=DIRECTION ( 'NONE',  ( 0.7071067811865463515, -0.7071067811865487940, 4.930380657631324879E-32 ) ) ;
#179300=CARTESIAN_POINT ( 'NONE',  ( -17.11825945287481687, 9.950000000011138823, -154.7500000000000284 ) ) ;
#179405=PLANE ( 'NONE',  #194002 ) ;
#179460=( LENGTH_UNIT ( ) NAMED_UNIT ( * ) SI_UNIT ( .MILLI., .METRE. ) );
#179464=ORIENTED_EDGE ( 'NONE', *, *, #185059, .F. ) ;
#179570=CARTESIAN_POINT ( 'NONE',  ( -16.81744102076749314, 9.950000000011142376, -146.6500000000000341 ) ) ;
#179764=EDGE_CURVE ( 'NONE', #71322, #157401, #93498, .T. ) ;
#180167=CARTESIAN_POINT ( 'NONE',  ( -16.91256925476571027, 9.985731158139333985, -146.5323575109947569 ) ) ;
#180190=CARTESIAN_POINT ( 'NONE',  ( -18.37013991200266005, 11.49974761622313224, -158.2930230105171461 ) ) ;
#180280=FACE_OUTER_BOUND ( 'NONE', #144927, .T. ) ;
#180463=VERTEX_POINT ( 'NONE', #195861 ) ;
#180600=ORIENTED_EDGE ( 'NONE', *, *, #234988, .T. ) ;
#180644=PLANE ( 'NONE',  #194063 ) ;
#180653=LINE ( 'NONE', #236754, #81389 ) ;
#180727=FACE_OUTER_BOUND ( 'NONE', #214206, .T. ) ;
#180731=CARTESIAN_POINT ( 'NONE',  ( -16.88219499860498374, 9.950206425438745228, -146.6493096901073443 ) ) ;
#180764=ORIENTED_EDGE ( 'NONE', *, *, #104725, .F. ) ;
#180831=ORIENTED_EDGE ( 'NONE', *, *, #120706, .F. ) ;
#181012=ADVANCED_FACE ( 'NONE', ( #68880 ), #145815, .T. ) ;
#181264=CARTESIAN_POINT ( 'NONE',  ( -16.89797118371713225, 9.976380722655967759, -154.9372933675581976 ) ) ;
#181476=CARTESIAN_POINT ( 'NONE',  ( 23.04999999999999716, 8.822561741677553471, -146.6500000000000341 ) ) ;
#181492=CARTESIAN_POINT ( 'NONE',  ( -23.25000000000000355, 5.650000000011139001, -146.6500000000000341 ) ) ;
#181583=EDGE_CURVE ( 'NONE', #184760, #56540, #193759, .T. ) ;
#181855=CARTESIAN_POINT ( 'NONE',  ( -14.11361717019516249, 9.457426452500060421, -152.5000418684000465 ) ) ;
#181898=ORIENTED_EDGE ( 'NONE', *, *, #78334, .F. ) ;
#182138=CARTESIAN_POINT ( 'NONE',  ( -20.65000000000000568, 7.250000000011138646, -143.2500000000000284 ) ) ;
#182184=ORIENTED_EDGE ( 'NONE', *, *, #193973, .T. ) ;
#182279=FACE_OUTER_BOUND ( 'NONE', #111563, .T. ) ;
#182749=CARTESIAN_POINT ( 'NONE',  ( 15.52844286134407881, 9.375669526436929857, -149.8677900093859705 ) ) ;
#183101=DIRECTION ( 'NONE',  ( 0.000000000000000000, 1.000000000000000000, -0.000000000000000000 ) ) ;
#183271=CARTESIAN_POINT ( 'NONE',  ( -33.72168855820452649, 11.47316190337362940, -158.2500000000000284 ) ) ;
#183286=DIRECTION ( 'NONE',  ( 1.000000000000000000, 0.000000000000000000, 0.000000000000000000 ) ) ;
#183357=CARTESIAN_POINT ( 'NONE',  ( 17.74533788810829904, 10.81849979148194763, -157.1863773250524616 ) ) ;
#183409=CARTESIAN_POINT ( 'NONE',  ( -16.79184697841823848, 9.948761661669548673, -146.6541422706025628 ) ) ;
#183508=CARTESIAN_POINT ( 'NONE',  ( -16.77683809663752257, 9.945835743215303282, -154.8360509808958057 ) ) ;
#183552=ORIENTED_EDGE ( 'NONE', *, *, #177271, .T. ) ;
#183611=ORIENTED_EDGE ( 'NONE', *, *, #70321, .F. ) ;
#184008=CARTESIAN_POINT ( 'NONE',  ( 12.60053434924910398, 9.389534562357857439, -149.6748093043899814 ) ) ;
#184140=EDGE_CURVE ( 'NONE', #157401, #235855, #97605, .T. ) ;
#184165=LINE ( 'NONE', #190298, #251204 ) ;
#184302=AXIS2_PLACEMENT_3D ( 'NONE', #173184, #251377, #235657 ) ;
#184440=CARTESIAN_POINT ( 'NONE',  ( -16.79139129368503802, 9.944944162472834748, -146.6702446328258134 ) ) ;
#184572=VECTOR ( 'NONE', #250861, 1000.000000000000000 ) ;
#184583=VECTOR ( 'NONE', #104451, 1000.000000000000000 ) ;
#184613=CARTESIAN_POINT ( 'NONE',  ( 15.57250062127603663, 9.370689921613768902, -151.5264651266610940 ) ) ;
#184760=VERTEX_POINT ( 'NONE', #31627 ) ;
#184855=CARTESIAN_POINT ( 'NONE',  ( -16.94445028196808778, 9.992063609708889516, -146.6073301784184935 ) ) ;
#185059=EDGE_CURVE ( 'NONE', #141855, #71313, #59831, .T. ) ;
#185401=CARTESIAN_POINT ( 'NONE',  ( -16.93935632781549572, 9.984730499736244269, -154.8896607487103267 ) ) ;
#185604=STYLED_ITEM ( 'NONE', ( #99865 ), #132346 ) ;
#185632=DIRECTION ( 'NONE',  ( 1.000000000000000000, 0.000000000000000000, -0.000000000000000000 ) ) ;
#185681=( BOUNDED_SURFACE ( )  B_SPLINE_SURFACE ( 3, 2, ( 
 ( #153330, #207188, #34648 ),
 ( #134980, #28592, #88480 ),
 ( #18905, #140124, #121884 ),
 ( #179300, #116725, #20210 ) ),
 .UNSPECIFIED., .F., .F., .F. ) 
 B_SPLINE_SURFACE_WITH_KNOTS ( ( 4, 4 ),
 ( 3, 3 ),
 ( 3.658908243880901523, 4.712388980384689674 ),
 ( 0.000000000000000000, 1.000000000000000000 ),
 .UNSPECIFIED. ) 
 GEOMETRIC_REPRESENTATION_ITEM ( )  RATIONAL_B_SPLINE_SURFACE ( (
 ( 1.000000000000000000, 0.8984936768950646524, 1.000000000000000000),
 ( 1.000000000000000000, 0.8646876308615526474, 1.000000000000000000),
 ( 1.000000000000000000, 0.7953136715913150523, 1.000000000000000000),
 ( 1.000000000000000000, 0.7071067811865475727, 1.000000000000000000) ) ) 
 REPRESENTATION_ITEM ( '' )  SURFACE ( )  );
#185898=CARTESIAN_POINT ( 'NONE',  ( 13.43663047529819998, 9.446645344706400493, -152.4108064561002607 ) ) ;
#185963=CARTESIAN_POINT ( 'NONE',  ( -21.65000000000000213, 7.250000000011138646, -154.8500000000000227 ) ) ;
#186101=ORIENTED_EDGE ( 'NONE', *, *, #53994, .T. ) ;
#186380=ORIENTED_EDGE ( 'NONE', *, *, #184140, .F. ) ;
#186440=CARTESIAN_POINT ( 'NONE',  ( -18.40000000000000213, 11.48667500176882861, -158.2500000000000284 ) ) ;
#186688=PLANE ( 'NONE',  #31536 ) ;
#186743=CARTESIAN_POINT ( 'NONE',  ( -16.89208623190940628, 9.951577948986638944, -154.8552722032183055 ) ) ;
#186920=CARTESIAN_POINT ( 'NONE',  ( 20.73486653747088582, 7.250000000011182166, -154.8500000000000227 ) ) ;
#187060=CIRCLE ( 'NONE', #141246, 0.09999999999999939493 ) ;
#187210=CARTESIAN_POINT ( 'NONE',  ( 12.68104795156995301, 9.396533993965077158, -151.9059397791733659 ) ) ;
#187254=EDGE_CURVE ( 'NONE', #49118, #11462, #207644, .T. ) ;
#187299=CARTESIAN_POINT ( 'NONE',  ( 23.24999999999999645, 8.822561741677553471, -154.8500000000000227 ) ) ;
#187388=ORIENTED_EDGE ( 'NONE', *, *, #11738, .T. ) ;
#187428=CARTESIAN_POINT ( 'NONE',  ( -16.94107738177415712, 10.01423928514777728, -146.5500000000000114 ) ) ;
#187491=ORIENTED_EDGE ( 'NONE', *, *, #138283, .T. ) ;
#187697=DIRECTION ( 'NONE',  ( -1.186688945009010077E-16, 1.000000000000000000, 0.000000000000000000 ) ) ;
#187726=ADVANCED_FACE ( 'NONE', ( #65392 ), #28889, .F. ) ;
#187728=CIRCLE ( 'NONE', #216910, 0.09999999999999939493 ) ;
#187894=CARTESIAN_POINT ( 'NONE',  ( -17.22361732159832215, 10.34515565861359221, -145.3707845258671512 ) ) ;
#188018=CARTESIAN_POINT ( 'NONE',  ( -16.88005004766534967, 9.950100503332199864, -154.8503361119487920 ) ) ;
#188028=ORIENTED_EDGE ( 'NONE', *, *, #139969, .F. ) ;
#188038=( BOUNDED_CURVE ( )  B_SPLINE_CURVE ( 3, ( #14769, #57697, #34332, #254604 ),
 .UNSPECIFIED., .F., .T. ) 
 B_SPLINE_CURVE_WITH_KNOTS ( ( 4, 4 ),
 ( 1.570796326794908992, 2.617993877991413587 ),
 .UNSPECIFIED. ) 
 CURVE ( )  GEOMETRIC_REPRESENTATION_ITEM ( )  RATIONAL_B_SPLINE_CURVE ( ( 1.000000000000000000, 0.9106836025229745335, 0.9106836025229745335, 1.000000000000000000 ) ) 
 REPRESENTATION_ITEM ( '' )  );
#188131=EDGE_CURVE ( 'NONE', #138980, #107290, #231617, .T. ) ;
#188221=CARTESIAN_POINT ( 'NONE',  ( -15.55912972643741199, 8.490870273573719373, -146.5500000000000114 ) ) ;
#188446=CARTESIAN_POINT ( 'NONE',  ( -16.87683809663752399, 9.950000000011137047, -154.0976359818037054 ) ) ;
#188876=ADVANCED_FACE ( 'NONE', ( #107125 ), #186688, .F. ) ;
#189168=DIRECTION ( 'NONE',  ( 1.000000000000000000, 0.000000000000000000, 0.000000000000000000 ) ) ;
#189694=PLANE ( 'NONE',  #86069 ) ;
#189760=EDGE_CURVE ( 'NONE', #134179, #180463, #70954, .T. ) ;
#189985=CARTESIAN_POINT ( 'NONE',  ( -16.93440969289731157, 9.995185175825108459, -146.5912341850108191 ) ) ;
#190071=ORIENTED_EDGE ( 'NONE', *, *, #61494, .F. ) ;
#190105=ORIENTED_EDGE ( 'NONE', *, *, #138444, .T. ) ;
#190149=VECTOR ( 'NONE', #129382, 1000.000000000000000 ) ;
#190159=CARTESIAN_POINT ( 'NONE',  ( -21.65000000000000213, 7.250000000011138646, -143.2500000000000284 ) ) ;
#190298=CARTESIAN_POINT ( 'NONE',  ( -23.25000000000000355, 11.75000000001113953, -143.2500000000000284 ) ) ;
#190313=ORIENTED_EDGE ( 'NONE', *, *, #37865, .F. ) ;
#190447=CARTESIAN_POINT ( 'NONE',  ( -33.72168855820452649, 23.65833333334447985, -150.7500000000000284 ) ) ;
#190472=VECTOR ( 'NONE', #132177, 1000.000000000000000 ) ;
#190478=DIRECTION ( 'NONE',  ( 1.186688945009009831E-16, -1.000000000000000000, 0.000000000000000000 ) ) ;
#190612=ADVANCED_FACE ( 'NONE', ( #74201 ), #96268, .F. ) ;
#190690=VERTEX_POINT ( 'NONE', #237085 ) ;
#191193=CARTESIAN_POINT ( 'NONE',  ( 23.04999999999999716, 8.822561741677553471, -143.2500000000000284 ) ) ;
#191402=CARTESIAN_POINT ( 'NONE',  ( -12.60206096961792177, 9.389686005666813884, -149.6728435063513132 ) ) ;
#191439=ORIENTED_EDGE ( 'NONE', *, *, #8490, .T. ) ;
#191568=DIRECTION ( 'NONE',  ( 0.7071067811865487940, 0.7071067811865462405, -7.215498431451186046E-16 ) ) ;
#191692=CARTESIAN_POINT ( 'NONE',  ( -16.80939487329395021, 9.950000000011138823, -154.8500000000009038 ) ) ;
#191724=AXIS2_PLACEMENT_3D ( 'NONE', #208393, #148406, #48002 ) ;
#191741=FACE_BOUND ( 'NONE', #221211, .T. ) ;
#191760=DIRECTION ( 'NONE',  ( 0.000000000000000000, 0.000000000000000000, -1.000000000000000000 ) ) ;
#191943=CARTESIAN_POINT ( 'NONE',  ( -16.93415306273742260, 9.995622260023671046, -154.9100569423604270 ) ) ;
#192060=CARTESIAN_POINT ( 'NONE',  ( -16.87036670365548474, 9.989418819312801290, -154.9795601173020714 ) ) ;
#192206=LINE ( 'NONE', #9689, #184572 ) ;
#192272=ORIENTED_EDGE ( 'NONE', *, *, #240429, .T. ) ;
#192439=CARTESIAN_POINT ( 'NONE',  ( -18.40000000000000213, 11.47316190337364183, -154.9500000000000455 ) ) ;
#192824=ORIENTED_EDGE ( 'NONE', *, *, #53617, .T. ) ;
#192909=ORIENTED_EDGE ( 'NONE', *, *, #92994, .F. ) ;
#193208=CARTESIAN_POINT ( 'NONE',  ( -16.93521499325732549, 9.994786119814676795, -154.9071085410935780 ) ) ;
#193229=EDGE_LOOP ( 'NONE', ( #46804, #151525, #24590 ) ) ;
#193759=B_SPLINE_CURVE_WITH_KNOTS ( 'NONE', 3,
 ( #103173, #82313, #124054, #204843, #184008, #66637, #221824, #44515, #241430, #203576, #201016, #161910, #107025, #27551, #146160, #225673, #47049, #43225, #5345, #122778, #126607, #223128, #182749, #62785, #41958, #164460 ),
 .UNSPECIFIED., .F., .F.,
 ( 4, 2, 2, 2, 2, 2, 2, 2, 2, 2, 2, 2, 4 ),
 ( 0.005476422646581339572, 0.006160811967703579139, 0.006845201288825817840, 0.007187395949386908567, 0.007529590609947999294, 0.007871785270509090021, 0.008213979931070179014, 0.008556174591631269741, 0.008898369252192360468, 0.009240563912753451195, 0.009582758573314541922, 0.01026714789443678062, 0.01095153721555902106 ),
 .UNSPECIFIED. ) ;
#193822=CARTESIAN_POINT ( 'NONE',  ( -23.25000000000000355, 5.650000000011139001, -154.8500000000000227 ) ) ;
#193849=EDGE_CURVE ( 'NONE', #88823, #138980, #152200, .T. ) ;
#193973=EDGE_CURVE ( 'NONE', #43985, #22565, #200260, .T. ) ;
#194002=AXIS2_PLACEMENT_3D ( 'NONE', #715, #159841, #17723 ) ;
#194063=AXIS2_PLACEMENT_3D ( 'NONE', #44985, #124529, #204046 ) ;
#194251=CARTESIAN_POINT ( 'NONE',  ( -16.79363873026997922, 9.948850229429586634, -154.8461537814455085 ) ) ;
#194339=PLANE ( 'NONE',  #37922 ) ;
#194369=CARTESIAN_POINT ( 'NONE',  ( 18.39999999999999147, 8.822561741677553471, -143.2500000000000284 ) ) ;
#194499=VERTEX_POINT ( 'NONE', #9447 ) ;
#194717=CARTESIAN_POINT ( 'NONE',  ( -16.97683809663752896, 9.950000000011140600, -147.2715247686699627 ) ) ;
#194889=CARTESIAN_POINT ( 'NONE',  ( -16.77431908686106610, 9.945805754529134290, -154.8358392176502605 ) ) ;
#195149=ORIENTED_EDGE ( 'NONE', *, *, #26837, .F. ) ;
#195248=CARTESIAN_POINT ( 'NONE',  ( -15.15766958671843945, 9.410538608540022665, -149.4326879971409596 ) ) ;
#195304=LINE ( 'NONE', #178304, #218367 ) ;
#195665=AXIS2_PLACEMENT_3D ( 'NONE', #97497, #196623, #16729 ) ;
#195774=CARTESIAN_POINT ( 'NONE',  ( 20.73486653747088937, 7.750000000011182166, -154.8500000000000227 ) ) ;
#195861=CARTESIAN_POINT ( 'NONE',  ( -18.40000000000000213, 11.75000000001113953, -158.2500000000000284 ) ) ;
#196096=ORIENTED_EDGE ( 'NONE', *, *, #41457, .F. ) ;
#196149=CARTESIAN_POINT ( 'NONE',  ( -16.80891096016325292, 9.950000000011137047, -154.8676628072681751 ) ) ;
#196173=CARTESIAN_POINT ( 'NONE',  ( -16.94107738177415357, 10.01423928514777728, -146.5500000000000114 ) ) ;
#196539=VECTOR ( 'NONE', #170058, 1000.000000000000000 ) ;
#196623=DIRECTION ( 'NONE',  ( 1.186688945009010077E-16, -1.000000000000000000, -0.000000000000000000 ) ) ;
#196807=ORIENTED_EDGE ( 'NONE', *, *, #165273, .T. ) ;
#196813=EDGE_CURVE ( 'NONE', #252467, #59289, #256250, .T. ) ;
#196888=CARTESIAN_POINT ( 'NONE',  ( -16.86422026484316916, 9.970447360871808939, -146.5822132256730299 ) ) ;
#196905=ADVANCED_FACE ( 'NONE', ( #1612 ), #105833, .F. ) ;
#197255=CARTESIAN_POINT ( 'NONE',  ( -16.89020380669786547, 9.950000000011137047, -146.7574111481105774 ) ) ;
#197352=ORIENTED_EDGE ( 'NONE', *, *, #37865, .T. ) ;
#197426=CARTESIAN_POINT ( 'NONE',  ( -16.84793658983431897, 9.950000000011140600, -154.7663533221900423 ) ) ;
#197535=ORIENTED_EDGE ( 'NONE', *, *, #246377, .T. ) ;
#197558=ORIENTED_EDGE ( 'NONE', *, *, #177641, .T. ) ;
#198102=EDGE_LOOP ( 'NONE', ( #121030, #224135, #257921, #135222, #99863, #121676, #7535, #160286, #192272, #7421 ) ) ;
#198175=CARTESIAN_POINT ( 'NONE',  ( -16.87368910959167678, 9.961273816702552963, -146.6124930966406339 ) ) ;
#198318=VERTEX_POINT ( 'NONE', #238543 ) ;
#198449=CARTESIAN_POINT ( 'NONE',  ( -17.27223548802645325, 10.34539739140118542, -156.1336061792111991 ) ) ;
#198721=CIRCLE ( 'NONE', #61353, 0.09999999999999939493 ) ;
#198838=CARTESIAN_POINT ( 'NONE',  ( -15.39126916658602795, 9.389571634557565716, -151.8176407123691547 ) ) ;
#199013=CLOSED_SHELL ( 'NONE', ( #187726, #125692, #3577, #136865, #136844, #133980, #105232, #196905, #190612, #74810, #7766, #132294, #66493, #64405, #5521, #9362, #107220, #57595, #155383, #257218, #60054, #110868, #247173, #26921, #212508, #104320, #214567, #188876, #8635, #104870, #92136, #91086, #173873, #138804, #68724, #202208, #215233, #237617, #21367, #75018, #160318, #237386, #102404, #95012, #250016, #173607, #68179, #120732, #106281, #43878, #25, #206531, #181012 ) ) ;
#199264=VERTEX_POINT ( 'NONE', #74420 ) ;
#199409=AXIS2_PLACEMENT_3D ( 'NONE', #94396, #115254, #30604 ) ;
#199484=DIRECTION ( 'NONE',  ( 1.186688945009010077E-16, -1.000000000000000000, -0.000000000000000000 ) ) ;
#199498=CARTESIAN_POINT ( 'NONE',  ( 20.27550659511089037, 9.216043722519994930, -154.8500000000000227 ) ) ;
#199546=CARTESIAN_POINT ( 'NONE',  ( -16.89318236219977365, 9.951535257886286345, -154.8551296321058715 ) ) ;
#199560=EDGE_LOOP ( 'NONE', ( #169679, #126258, #154546, #213492 ) ) ;
#199629=VERTEX_POINT ( 'NONE', #174520 ) ;
#199763=CARTESIAN_POINT ( 'NONE',  ( -16.94107738177414291, 10.01423928514777728, -154.9500000000000455 ) ) ;
#200076=DIRECTION ( 'NONE',  ( 0.000000000000000000, 0.000000000000000000, 1.000000000000000000 ) ) ;
#200135=CARTESIAN_POINT ( 'NONE',  ( -15.57281606413133090, 9.370655051134637148, -151.5258232559808675 ) ) ;
#200217=DIRECTION ( 'NONE',  ( -1.020425574104004196E-15, 0.000000000000000000, 1.000000000000000000 ) ) ;
#200260=CIRCLE ( 'NONE', #33720, 1.749999999999999778 ) ;
#200287=CARTESIAN_POINT ( 'NONE',  ( -16.89060415895970735, 9.951220762813354881, -146.6459202242704691 ) ) ;
#200595=B_SPLINE_CURVE_WITH_KNOTS ( 'NONE', 3,
 ( #32401, #93624, #114469, #134022, #229295, #31125, #209725, #74096, #153657, #91058 ),
 .UNSPECIFIED., .F., .F.,
 ( 4, 2, 2, 2, 4 ),
 ( 5.247129907028296623E-16, 9.930191194499898442E-05, 0.0001986038238894732421, 0.0003972076477784217846, 0.0007944152955563189237 ),
 .UNSPECIFIED. ) ;
#200685=FACE_OUTER_BOUND ( 'NONE', #27228, .T. ) ;
#200765=LINE ( 'NONE', #101621, #121997 ) ;
#201005=CARTESIAN_POINT ( 'NONE',  ( -17.27223548802547626, 10.34539739140569381, -145.3663938207882609 ) ) ;
#201016=CARTESIAN_POINT ( 'NONE',  ( 13.54556439290363912, 9.450592112144859058, -149.0561883188084096 ) ) ;
#201118=CARTESIAN_POINT ( 'NONE',  ( -16.83558968593869665, 9.950000000011137047, -146.6623051876167381 ) ) ;
#201222=CARTESIAN_POINT ( 'NONE',  ( 21.72449340488910252, 10.28395627750227703, -146.6500000000000341 ) ) ;
#201279=VECTOR ( 'NONE', #35663, 1000.000000000000000 ) ;
#201404=CARTESIAN_POINT ( 'NONE',  ( -15.73854595235691889, 9.351413679112544841, -150.9803435675489709 ) ) ;
#201435=CARTESIAN_POINT ( 'NONE',  ( -16.83794237512073622, 9.926359221118632448, -146.8035421586989742 ) ) ;
#201469=VERTEX_POINT ( 'NONE', #120370 ) ;
#201673=CARTESIAN_POINT ( 'NONE',  ( -16.77828822508139694, 9.946229374931901290, -146.6626282513739739 ) ) ;
#201697=PRODUCT_DEFINITION_SHAPE ( 'NONE', 'NONE',  #70844 ) ;
#201829=CARTESIAN_POINT ( 'NONE',  ( -16.94275863009466576, 9.989496048673542461, -146.6083026179589126 ) ) ;
#201844=ORIENTED_EDGE ( 'NONE', *, *, #70321, .T. ) ;
#202155=CIRCLE ( 'NONE', #39858, 0.9000000000000014655 ) ;
#202208=ADVANCED_FACE ( 'NONE', ( #90924 ), #70116, .T. ) ;
#202403=CARTESIAN_POINT ( 'NONE',  ( -16.84793658983432252, 9.950000000011138823, -146.7336466778100430 ) ) ;
#202408=APPLICATION_CONTEXT ( 'automotive_design' ) ;
#202648=ORIENTED_EDGE ( 'NONE', *, *, #161250, .F. ) ;
#202691=CARTESIAN_POINT ( 'NONE',  ( -14.22969084473441370, 9.456007326080465347, -152.4886334941467965 ) ) ;
#202896=CARTESIAN_POINT ( 'NONE',  ( 12.25000000000000000, 9.350000000011140955, -150.7500000000000284 ) ) ;
#202955=CARTESIAN_POINT ( 'NONE',  ( -16.77732147278574715, 9.945966932584589415, -146.6635087568758422 ) ) ;
#203195=ORIENTED_EDGE ( 'NONE', *, *, #179764, .T. ) ;
#203266=VERTEX_POINT ( 'NONE', #151299 ) ;
#203292=PRODUCT_CONTEXT ( 'NONE', #248882, 'mechanical' ) ;
#203363=VERTEX_POINT ( 'NONE', #38717 ) ;
#203377=FACE_OUTER_BOUND ( 'NONE', #103461, .T. ) ;
#203397=ORIENTED_EDGE ( 'NONE', *, *, #8490, .F. ) ;
#203446=ORIENTED_EDGE ( 'NONE', *, *, #163565, .F. ) ;
#203576=CARTESIAN_POINT ( 'NONE',  ( 13.43443725621852636, 9.446557523083688679, -149.0899419543459032 ) ) ;
#203592=CARTESIAN_POINT ( 'NONE',  ( 17.23472005113828232, 10.30788195451192379, -145.4534231399313740 ) ) ;
#203915=VECTOR ( 'NONE', #38469, 1000.000000000000000 ) ;
#204009=CARTESIAN_POINT ( 'NONE',  ( 18.39999999999999503, 11.75000000001113953, -154.8500000000000227 ) ) ;
#204046=DIRECTION ( 'NONE',  ( -1.000000000000000000, 0.000000000000000000, 1.073024830501117725E-15 ) ) ;
#204120=SURFACE_SIDE_STYLE ('',( #102429 ) ) ;
#204165=CARTESIAN_POINT ( 'NONE',  ( 13.54577453029516931, 9.450602096099684601, -152.4438959630967645 ) ) ;
#204293=CARTESIAN_POINT ( 'NONE',  ( -18.40000000000000213, 11.47316190337364183, -158.1740539331920559 ) ) ;
#204384=CARTESIAN_POINT ( 'NONE',  ( -16.94389599338512298, 9.991197989766199328, -146.6076448018102667 ) ) ;
#204634=CARTESIAN_POINT ( 'NONE',  ( -16.92570016628984675, 9.958788957751012916, -154.8793493299610304 ) ) ;
#204799=ORIENTED_EDGE ( 'NONE', *, *, #245388, .F. ) ;
#204830=SURFACE_STYLE_FILL_AREA ( #82298 ) ;
#204843=CARTESIAN_POINT ( 'NONE',  ( 12.47034474403013071, 9.375538102059163492, -149.8698758809908611 ) ) ;
#205012=ORIENTED_EDGE ( 'NONE', *, *, #156647, .T. ) ;
#205187=DIRECTION ( 'NONE',  ( -0.000000000000000000, -0.000000000000000000, -1.000000000000000000 ) ) ;
#205328=ORIENTED_EDGE ( 'NONE', *, *, #135002, .T. ) ;
#205451=CARTESIAN_POINT ( 'NONE',  ( 15.31784899511109010, 9.396630376328873879, -151.9070573928183592 ) ) ;
#205572=VECTOR ( 'NONE', #232275, 999.9999999999998863 ) ;
#205667=CARTESIAN_POINT ( 'NONE',  ( -16.91247567987037570, 9.959082683680401615, -146.6287244585373628 ) ) ;
#205710=DIRECTION ( 'NONE',  ( 1.186688945009010077E-16, -1.000000000000000000, -0.000000000000000000 ) ) ;
#206102=FACE_OUTER_BOUND ( 'NONE', #244487, .T. ) ;
#206531=ADVANCED_FACE ( 'NONE', ( #94586 ), #185681, .T. ) ;
#206656=VERTEX_POINT ( 'NONE', #167444 ) ;
#206697=DIRECTION ( 'NONE',  ( 0.000000000000000000, -1.000000000000000000, 0.000000000000000000 ) ) ;
#207004=ORIENTED_EDGE ( 'NONE', *, *, #55725, .F. ) ;
#207052=VERTEX_POINT ( 'NONE', #105826 ) ;
#207188=CARTESIAN_POINT ( 'NONE',  ( -16.91049119928363353, 9.950000000011137047, -154.8817203931908182 ) ) ;
#207231=CARTESIAN_POINT ( 'NONE',  ( -18.38639463286148867, 11.48019957384713230, -143.2500000000000284 ) ) ;
#207329=CARTESIAN_POINT ( 'NONE',  ( -18.40000000000000213, 11.47316190337362940, -146.6085786437627121 ) ) ;
#207474=EDGE_CURVE ( 'NONE', #23667, #88823, #161539, .T. ) ;
#207532=AXIS2_PLACEMENT_3D ( 'NONE', #77090, #36721, #75816 ) ;
#207541=ORIENTED_EDGE ( 'NONE', *, *, #162397, .T. ) ;
#207644=LINE ( 'NONE', #68116, #231267 ) ;
#207722=CARTESIAN_POINT ( 'NONE',  ( -20.65000000000000568, 5.650000000011139001, -154.8500000000000227 ) ) ;
#207958=ORIENTED_EDGE ( 'NONE', *, *, #188131, .F. ) ;
#208393=CARTESIAN_POINT ( 'NONE',  ( -23.25000000000000355, 10.05000000001113847, -154.7500000000000284 ) ) ;
#208428=LINE ( 'NONE', #91022, #256162 ) ;
#208614=ORIENTED_EDGE ( 'NONE', *, *, #84462, .F. ) ;
#208796=DIRECTION ( 'NONE',  ( -1.000000000000000000, 1.652117596168391700E-15, 0.000000000000000000 ) ) ;
#209017=VERTEX_POINT ( 'NONE', #126204 ) ;
#209056=LINE ( 'NONE', #130795, #132121 ) ;
#209272=VERTEX_POINT ( 'NONE', #236858 ) ;
#209725=CARTESIAN_POINT ( 'NONE',  ( -16.94226253665225812, 9.950000000011138823, -154.5532654043842626 ) ) ;
#209908=CIRCLE ( 'NONE', #89082, 14.30833333333333890 ) ;
#209917=ORIENTED_EDGE ( 'NONE', *, *, #210093, .F. ) ;
#210067=CARTESIAN_POINT ( 'NONE',  ( 21.13736287352038445, 8.046642376395153562, -154.8500000000000227 ) ) ;
#210093=EDGE_CURVE ( 'NONE', #203266, #235855, #1158, .T. ) ;
#210204=CARTESIAN_POINT ( 'NONE',  ( -16.94445028196807002, 9.992063609708893068, -154.8926698215815634 ) ) ;
#210713=CARTESIAN_POINT ( 'NONE',  ( 18.39999999999999503, 11.47316190337363828, -154.8500000000000227 ) ) ;
#210758=DIRECTION ( 'NONE',  ( 0.8049926720990051576, 0.5932847527679298016, -0.000000000000000000 ) ) ;
#210764=VECTOR ( 'NONE', #178812, 1000.000000000000000 ) ;
#210819=ORIENTED_EDGE ( 'NONE', *, *, #28276, .T. ) ;
#210829=ORIENTED_EDGE ( 'NONE', *, *, #235136, .T. ) ;
#211191=DIRECTION ( 'NONE',  ( -0.000000000000000000, 0.000000000000000000, -1.000000000000000000 ) ) ;
#211223=VECTOR ( 'NONE', #69039, 1000.000000000000000 ) ;
#211425=CARTESIAN_POINT ( 'NONE',  ( -16.88328101497759448, 9.950352834230013599, -154.8511795149292993 ) ) ;
#211440=EDGE_CURVE ( 'NONE', #59289, #1366, #150631, .T. ) ;
#211591=EDGE_LOOP ( 'NONE', ( #82240, #15169, #224972, #231675 ) ) ;
#211797=FACE_OUTER_BOUND ( 'NONE', #198102, .T. ) ;
#211942=VECTOR ( 'NONE', #247585, 999.9999999999998863 ) ;
#211947=ORIENTED_EDGE ( 'NONE', *, *, #176278, .T. ) ;
#212042=CARTESIAN_POINT ( 'NONE',  ( -16.27683809663750480, 9.350000000011133849, -154.9500000000000455 ) ) ;
#212145=CARTESIAN_POINT ( 'NONE',  ( -18.40000000000000213, 11.48667500176882861, -158.2500000000000284 ) ) ;
#212185=CARTESIAN_POINT ( 'NONE',  ( 15.48841904831874849, 8.561580951692381092, -154.8500000000000227 ) ) ;
#212235=CARTESIAN_POINT ( 'NONE',  ( -13.43673303185029688, 9.446648990640015953, -149.0891632959232140 ) ) ;
#212313=DIRECTION ( 'NONE',  ( 0.000000000000000000, 1.000000000000000000, 0.000000000000000000 ) ) ;
#212338=CIRCLE ( 'NONE', #37360, 0.09999999999998898659 ) ;
#212442=( BOUNDED_CURVE ( )  B_SPLINE_CURVE ( 3, ( #223736, #146751, #183357, #45118 ),
 .UNSPECIFIED., .F., .F. ) 
 B_SPLINE_CURVE_WITH_KNOTS ( ( 4, 4 ),
 ( 3.432212674861196522, 3.693332928900581624 ),
 .UNSPECIFIED. ) 
 CURVE ( )  GEOMETRIC_REPRESENTATION_ITEM ( )  RATIONAL_B_SPLINE_CURVE ( ( 1.000000000000000000, 0.9943260843901261525, 0.9943260843901261525, 1.000000000000000000 ) ) 
 REPRESENTATION_ITEM ( '' )  );
#212508=ADVANCED_FACE ( 'NONE', ( #84334 ), #226443, .F. ) ;
#212523=CYLINDRICAL_SURFACE ( 'NONE', #86721, 0.5000000000000004441 ) ;
#212637=EDGE_CURVE ( 'NONE', #45717, #207052, #170404, .T. ) ;
#212672=VERTEX_POINT ( 'NONE', #9992 ) ;
#212733=CARTESIAN_POINT ( 'NONE',  ( -18.35668295345803713, 11.47316190337362940, -158.2500000000000284 ) ) ;
#212845=CARTESIAN_POINT ( 'NONE',  ( 22.88900146558018989, 8.703904791123973084, -143.2500000000000284 ) ) ;
#213136=LINE ( 'NONE', #50199, #68856 ) ;
#213178=CARTESIAN_POINT ( 'NONE',  ( 20.04999999999999716, 8.750000000011173285, -154.8500000000000227 ) ) ;
#213404=EDGE_CURVE ( 'NONE', #256073, #134179, #218758, .T. ) ;
#213490=CARTESIAN_POINT ( 'NONE',  ( -12.29659703204451837, 9.355888454513703323, -150.2886428967780148 ) ) ;
#213492=ORIENTED_EDGE ( 'NONE', *, *, #70285, .F. ) ;
#213507=FACE_OUTER_BOUND ( 'NONE', #154700, .T. ) ;
#213632=CARTESIAN_POINT ( 'NONE',  ( 20.09999999999999787, 9.750000000011137757, -146.6500000000000341 ) ) ;
#213837=ORIENTED_EDGE ( 'NONE', *, *, #222801, .T. ) ;
#213939=CARTESIAN_POINT ( 'NONE',  ( -16.92778301347272674, 10.00094491684634690, -146.5714818920313860 ) ) ;
#214043=CARTESIAN_POINT ( 'NONE',  ( -16.93211319090181988, 9.999986781168624717, -154.9225054992730861 ) ) ;
#214111=ORIENTED_EDGE ( 'NONE', *, *, #177271, .F. ) ;
#214129=FACE_OUTER_BOUND ( 'NONE', #26864, .T. ) ;
#214206=EDGE_LOOP ( 'NONE', ( #190105, #52319, #146772, #192824 ) ) ;
#214419=CARTESIAN_POINT ( 'NONE',  ( -16.83558968593874638, 9.950000000011137047, -154.8376948123833188 ) ) ;
#214447=LINE ( 'NONE', #76217, #26217 ) ;
#214567=ADVANCED_FACE ( 'NONE', ( #176218 ), #92794, .F. ) ;
#214850=CARTESIAN_POINT ( 'NONE',  ( 20.99999999999999645, 9.750000000011137757, -146.6500000000000341 ) ) ;
#214868=EDGE_CURVE ( 'NONE', #1028, #56540, #126492, .T. ) ;
#215198=EDGE_CURVE ( 'NONE', #225332, #221934, #156362, .T. ) ;
#215233=ADVANCED_FACE ( 'NONE', ( #144434 ), #227847, .F. ) ;
#215623=CARTESIAN_POINT ( 'NONE',  ( -18.40000000000000213, 11.47316190337362762, -146.6500000000000341 ) ) ;
#215790=EDGE_LOOP ( 'NONE', ( #89077, #7248, #63002, #76709 ) ) ;
#216165=LINE ( 'NONE', #37558, #166068 ) ;
#216288=DIRECTION ( 'NONE',  ( 1.000000000000000000, -0.000000000000000000, -0.000000000000000000 ) ) ;
#216910=AXIS2_PLACEMENT_3D ( 'NONE', #153760, #139240, #237091 ) ;
#217391=ORIENTED_EDGE ( 'NONE', *, *, #155118, .F. ) ;
#217779=VERTEX_POINT ( 'NONE', #158312 ) ;
#217846=LINE ( 'NONE', #3956, #84409 ) ;
#218082=CARTESIAN_POINT ( 'NONE',  ( -16.94225986326250322, 9.950000000011138823, -146.9467193756078700 ) ) ;
#218225=LINE ( 'NONE', #254762, #157308 ) ;
#218367=VECTOR ( 'NONE', #175737, 1000.000000000000000 ) ;
#218385=CARTESIAN_POINT ( 'NONE',  ( -12.92414019175887319, 9.417632963117446465, -152.1489484657323032 ) ) ;
#218540=SURFACE_STYLE_USAGE ( .BOTH. , #204120 ) ;
#218599=DIRECTION ( 'NONE',  ( 1.000000000000000000, 0.000000000000000000, 0.000000000000000000 ) ) ;
#218698=LINE ( 'NONE', #25660, #245389 ) ;
#218758=B_SPLINE_CURVE_WITH_KNOTS ( 'NONE', 3,
 ( #133187, #212733, #34124, #113618, #94046, #17111, #253112 ),
 .UNSPECIFIED., .F., .F.,
 ( 4, 3, 4 ),
 ( 0.000000000000000000, 3.882884552234471334E-05, 5.798605692158473166E-05 ),
 .UNSPECIFIED. ) ;
#218896=ORIENTED_EDGE ( 'NONE', *, *, #29348, .F. ) ;
#219065=CARTESIAN_POINT ( 'NONE',  ( -16.94107738177414291, 10.01423928514777373, -154.9500000000000455 ) ) ;
#219262=FILL_AREA_STYLE_COLOUR ( '', #237337 ) ;
#219292=CARTESIAN_POINT ( 'NONE',  ( -18.44085059012131822, 11.51401249349495970, -158.2403053191215463 ) ) ;
#219434=CIRCLE ( 'NONE', #252761, 0.1999999999999987899 ) ;
#219542=ORIENTED_EDGE ( 'NONE', *, *, #23563, .F. ) ;
#219747=EDGE_CURVE ( 'NONE', #156798, #221299, #208428, .T. ) ;
#219813=AXIS2_PLACEMENT_3D ( 'NONE', #213178, #72416, #151958 ) ;
#219838=CARTESIAN_POINT ( 'NONE',  ( -16.89268316805466341, 9.951721813253341153, -146.6442475214544743 ) ) ;
#220396=DIRECTION ( 'NONE',  ( 0.000000000000000000, 0.000000000000000000, 1.000000000000000000 ) ) ;
#220688=CARTESIAN_POINT ( 'NONE',  ( -16.96982749440708460, 9.950000000011137047, -147.1247784088109256 ) ) ;
#220835=VERTEX_POINT ( 'NONE', #242418 ) ;
#221134=DIRECTION ( 'NONE',  ( 0.2834754621636358940, -0.2834754621636437211, 0.9161240771326893961 ) ) ;
#221211=EDGE_LOOP ( 'NONE', ( #164746, #183552 ) ) ;
#221299=VERTEX_POINT ( 'NONE', #187299 ) ;
#221370=CARTESIAN_POINT ( 'NONE',  ( -16.90257928357874562, 9.954106821116520010, -146.6362854301137020 ) ) ;
#221567=CARTESIAN_POINT ( 'NONE',  ( -16.86757978335471364, 9.965650379045438712, -146.5980046531675498 ) ) ;
#221821=CARTESIAN_POINT ( 'NONE',  ( -16.94107738177415712, 10.01423928514777728, -146.5500000000000114 ) ) ;
#221824=CARTESIAN_POINT ( 'NONE',  ( 12.93225390519045703, 9.417651958852161442, -149.3587873924404619 ) ) ;
#221838=CARTESIAN_POINT ( 'NONE',  ( -12.25000000000000178, 9.850000000011133849, -150.7500000000000284 ) ) ;
#221934=VERTEX_POINT ( 'NONE', #127669 ) ;
#221938=VERTEX_POINT ( 'NONE', #126375 ) ;
#222257=CARTESIAN_POINT ( 'NONE',  ( -16.80468759584937288, 9.942153675145293690, -146.6900188662016546 ) ) ;
#222377=CARTESIAN_POINT ( 'NONE',  ( -16.87435696428308063, 9.950002462943377424, -146.6499917651665896 ) ) ;
#222602=CARTESIAN_POINT ( 'NONE',  ( -16.85312964099708566, 9.913604682078865693, -154.6028157064305049 ) ) ;
#222801=EDGE_CURVE ( 'NONE', #254838, #201469, #61940, .T. ) ;
#222848=EDGE_CURVE ( 'NONE', #235855, #156630, #4515, .T. ) ;
#223053=( BOUNDED_SURFACE ( )  B_SPLINE_SURFACE ( 3, 2, ( 
 ( #87423, #126568, #165714 ),
 ( #5296, #242647, #245238 ),
 ( #66598, #101832, #225631 ),
 ( #144826, #146121, #82265 ) ),
 .UNSPECIFIED., .F., .F., .F. ) 
 B_SPLINE_SURFACE_WITH_KNOTS ( ( 4, 4 ),
 ( 3, 3 ),
 ( 4.712388980384689674, 5.765869716888459173 ),
 ( 0.000000000000000000, 1.000000000000000000 ),
 .UNSPECIFIED. ) 
 GEOMETRIC_REPRESENTATION_ITEM ( )  RATIONAL_B_SPLINE_SURFACE ( (
 ( 1.000000000000000000, 0.7071067811865475727, 1.000000000000000000),
 ( 1.000000000000000000, 0.7953136715913045052, 1.000000000000000000),
 ( 1.000000000000000000, 0.8646876308615548679, 1.000000000000000000),
 ( 1.000000000000000000, 0.8984936768950610997, 1.000000000000000000) ) ) 
 REPRESENTATION_ITEM ( '' )  SURFACE ( )  );
#223114=( NAMED_UNIT ( * ) PLANE_ANGLE_UNIT ( ) SI_UNIT ( $, .RADIAN. ) );
#223128=CARTESIAN_POINT ( 'NONE',  ( 15.39793903038208178, 9.389686005666810331, -149.6728435063513132 ) ) ;
#223145=EDGE_CURVE ( 'NONE', #123340, #81862, #255927, .T. ) ;
#223675=CARTESIAN_POINT ( 'NONE',  ( -23.25000000000000355, 5.650000000011139001, -143.2500000000000284 ) ) ;
#223727=CARTESIAN_POINT ( 'NONE',  ( 12.30626653967341255, 9.356790025057035720, -151.2048265086139054 ) ) ;
#223736=CARTESIAN_POINT ( 'NONE',  ( 16.87683809663749557, 9.950000000011131718, -154.8500000000000227 ) ) ;
#223896=CARTESIAN_POINT ( 'NONE',  ( -16.83794479845801106, 9.926357419362647150, -154.6964447042223014 ) ) ;
#223947=CARTESIAN_POINT ( 'NONE',  ( -16.93658623642901873, 9.980381671668284937, -146.6119027291292127 ) ) ;
#223955=CARTESIAN_POINT ( 'NONE',  ( -17.11825945287481332, 10.05000000001113847, -154.8500000000000227 ) ) ;
#223960=ORIENTED_EDGE ( 'NONE', *, *, #41457, .T. ) ;
#224135=ORIENTED_EDGE ( 'NONE', *, *, #227888, .T. ) ;
#224172=EDGE_CURVE ( 'NONE', #166383, #151298, #149085, .T. ) ;
#224526=CARTESIAN_POINT ( 'NONE',  ( -16.77180007708460252, 9.950000000011137047, -146.6356141189548339 ) ) ;
#224663=ORIENTED_EDGE ( 'NONE', *, *, #193849, .T. ) ;
#224972=ORIENTED_EDGE ( 'NONE', *, *, #219747, .T. ) ;
#225006=EDGE_LOOP ( 'NONE', ( #44983, #192909, #36869, #69152 ) ) ;
#225332=VERTEX_POINT ( 'NONE', #253195 ) ;
#225479=ORIENTED_EDGE ( 'NONE', *, *, #23563, .T. ) ;
#225631=CARTESIAN_POINT ( 'NONE',  ( -16.97092634996681682, 10.00088896635984881, -146.6301427662976096 ) ) ;
#225673=CARTESIAN_POINT ( 'NONE',  ( 14.45204356427542258, 9.450668889178682974, -149.0555464902073481 ) ) ;
#225761=DIRECTION ( 'NONE',  ( 0.000000000000000000, -1.000000000000000000, 0.000000000000000000 ) ) ;
#225779=LINE ( 'NONE', #47139, #46057 ) ;
#225785=CARTESIAN_POINT ( 'NONE',  ( -16.90987985657661952, 9.957807518190888274, -154.8692870888836808 ) ) ;
#225791=VERTEX_POINT ( 'NONE', #79380 ) ;
#226082=DIRECTION ( 'NONE',  ( -0.7071067811865463515, 0.7071067811865487940, -0.000000000000000000 ) ) ;
#226118=DIRECTION ( 'NONE',  ( -1.000000000000000000, 0.000000000000000000, -1.020425574104004196E-15 ) ) ;
#226394=CARTESIAN_POINT ( 'NONE',  ( -17.78043020864321022, 10.85359211201684460, -157.1630491657202526 ) ) ;
#226400=EDGE_LOOP ( 'NONE', ( #166486, #146967, #136299, #111582 ) ) ;
#226443=PLANE ( 'NONE',  #94724 ) ;
#226612=EDGE_LOOP ( 'NONE', ( #219542, #61163, #240925, #97894, #82984 ) ) ;
#226856=VERTEX_POINT ( 'NONE', #178770 ) ;
#226921=DIRECTION ( 'NONE',  ( -1.000000000000000000, 0.000000000000000000, 0.000000000000000000 ) ) ;
#227291=( GEOMETRIC_REPRESENTATION_CONTEXT ( 3 ) GLOBAL_UNCERTAINTY_ASSIGNED_CONTEXT ( ( #66086 ) ) GLOBAL_UNIT_ASSIGNED_CONTEXT ( ( #179460, #84129, #43781 ) ) REPRESENTATION_CONTEXT ( 'NONE', 'WORKASPACE' ) );
#227377=ORIENTED_EDGE ( 'NONE', *, *, #251041, .F. ) ;
#227638=ORIENTED_EDGE ( 'NONE', *, *, #139969, .T. ) ;
#227759=CARTESIAN_POINT ( 'NONE',  ( -16.85939681242906474, 9.905225185936462395, -154.5399219551915451 ) ) ;
#227816=CARTESIAN_POINT ( 'NONE',  ( -16.93906926870270624, 10.01214687095770906, -146.5534523072268485 ) ) ;
#227847=CYLINDRICAL_SURFACE ( 'NONE', #53756, 1.749999999999998002 ) ;
#227888=EDGE_CURVE ( 'NONE', #10139, #5552, #31108, .T. ) ;
#227947=PLANE ( 'NONE',  #173838 ) ;
#228056=CARTESIAN_POINT ( 'NONE',  ( -15.55912972643740488, 8.490870273573721150, -154.8500000000000227 ) ) ;
#228327=VECTOR ( 'NONE', #4614, 1000.000000000000000 ) ;
#228390=CARTESIAN_POINT ( 'NONE',  ( -16.93301857435213620, 9.976309354746611291, -154.8857755711614459 ) ) ;
#228404=CARTESIAN_POINT ( 'NONE',  ( 20.73486653747090003, 7.250000000011182166, -154.8500000000000227 ) ) ;
#228612=CARTESIAN_POINT ( 'NONE',  ( -16.87304349924914604, 9.961745077968330975, -154.8890666750452567 ) ) ;
#228627=PLANE ( 'NONE',  #74375 ) ;
#229004=CARTESIAN_POINT ( 'NONE',  ( -18.40000000000000213, 11.33174054713633261, -154.8500000000000227 ) ) ;
#229018=FACE_OUTER_BOUND ( 'NONE', #138597, .T. ) ;
#229153=B_SPLINE_CURVE_WITH_KNOTS ( 'NONE', 3,
 ( #164010, #4896, #243533, #28382, #64888, #232984, #150854, #189985, #54307, #169169, #153476, #32215, #51724, #131289, #173036, #227816, #109144, #133856, #187428 ),
 .UNSPECIFIED., .F., .F.,
 ( 4, 3, 3, 3, 3, 3, 4 ),
 ( 0.0001624081864585664764, 0.0001685232196531825368, 0.0001764526673566942224, 0.0001916878551483208173, 0.0002009890782182613455, 0.0002238845907555189795, 0.0002283406619926576847 ),
 .UNSPECIFIED. ) ;
#229239=ORIENTED_EDGE ( 'NONE', *, *, #242423, .T. ) ;
#229291=EDGE_LOOP ( 'NONE', ( #82415, #168153, #91243, #197558 ) ) ;
#229295=CARTESIAN_POINT ( 'NONE',  ( -16.90138253750126651, 9.950000000011137047, -154.7115627079046192 ) ) ;
#229359=CARTESIAN_POINT ( 'NONE',  ( -18.35663730107557257, 11.47390742652235573, -143.2500000000000284 ) ) ;
#229653=ORIENTED_EDGE ( 'NONE', *, *, #54134, .F. ) ;
#229668=CARTESIAN_POINT ( 'NONE',  ( -16.92563707711778065, 9.968990694407935393, -154.8807582995239898 ) ) ;
#230501=CARTESIAN_POINT ( 'NONE',  ( -13.22483237240079568, 9.436674251854009654, -149.1768619309992232 ) ) ;
#230591=DIRECTION ( 'NONE',  ( -1.000000000000000000, -1.646408749285562691E-14, 0.000000000000000000 ) ) ;
#231032=VECTOR ( 'NONE', #143250, 1000.000000000000000 ) ;
#231056=LINE ( 'NONE', #73278, #63402 ) ;
#231141=DIRECTION ( 'NONE',  ( -1.000000000000000000, 0.000000000000000000, 0.000000000000000000 ) ) ;
#231202=EDGE_LOOP ( 'NONE', ( #106629, #29998, #180600, #173140 ) ) ;
#231214=CARTESIAN_POINT ( 'NONE',  ( 20.27550659511089037, 9.216043722520002035, -154.8500000000000227 ) ) ;
#231221=DIRECTION ( 'NONE',  ( 0.7071067811865474617, 0.7071067811865474617, 0.000000000000000000 ) ) ;
#231267=VECTOR ( 'NONE', #4270, 1000.000000000000000 ) ;
#231546=VECTOR ( 'NONE', #43443, 999.9999999999998863 ) ;
#231584=FACE_OUTER_BOUND ( 'NONE', #120755, .T. ) ;
#231617=CIRCLE ( 'NONE', #94223, 0.09999999999999602263 ) ;
#231675=ORIENTED_EDGE ( 'NONE', *, *, #24217, .T. ) ;
#231794=CARTESIAN_POINT ( 'NONE',  ( -15.39946565075089957, 9.389534562357857439, -149.6748093043899814 ) ) ;
#231813=DIRECTION ( 'NONE',  ( 0.000000000000000000, -0.000000000000000000, -1.000000000000000000 ) ) ;
#231973=CARTESIAN_POINT ( 'NONE',  ( -16.27683809663751191, 9.350000000011133849, -143.2500000000000000 ) ) ;
#232171=FACE_OUTER_BOUND ( 'NONE', #173813, .T. ) ;
#232243=CARTESIAN_POINT ( 'NONE',  ( -16.94107738177415712, 10.01423928514777550, -146.5500000000000114 ) ) ;
#232275=DIRECTION ( 'NONE',  ( 0.5932847527679299127, -0.8049926720990051576, 6.366092712777055223E-16 ) ) ;
#232280=ORIENTED_EDGE ( 'NONE', *, *, #149992, .T. ) ;
#232731=CARTESIAN_POINT ( 'NONE',  ( -16.87998658237741978, 9.950000000011137047, -154.6363604322605454 ) ) ;
#232984=CARTESIAN_POINT ( 'NONE',  ( -16.93772744219066340, 9.993541108763512426, -146.5980619719697415 ) ) ;
#233035=DIRECTION ( 'NONE',  ( 1.000000000000000000, 1.186688945009009831E-16, 0.000000000000000000 ) ) ;
#233089=CARTESIAN_POINT ( 'NONE',  ( -13.77178122865953824, 9.456028260519072859, -149.0111980350657745 ) ) ;
#233209=DIRECTION ( 'NONE',  ( -0.000000000000000000, -0.000000000000000000, -1.000000000000000000 ) ) ;
#233297=EDGE_LOOP ( 'NONE', ( #27836, #66495, #239631, #56388, #40347 ) ) ;
#233361=AXIS2_PLACEMENT_3D ( 'NONE', #59466, #221134, #60777 ) ;
#233380=DIRECTION ( 'NONE',  ( 1.186688945009010077E-16, -1.000000000000000000, -0.000000000000000000 ) ) ;
#233588=VECTOR ( 'NONE', #105849, 1000.000000000000000 ) ;
#233601=DIRECTION ( 'NONE',  ( 1.000000000000000000, 0.000000000000000000, 0.000000000000000000 ) ) ;
#233615=CARTESIAN_POINT ( 'NONE',  ( -16.93262454970419384, 10.00202046794151478, -154.9270762262373182 ) ) ;
#233779=FACE_OUTER_BOUND ( 'NONE', #226612, .T. ) ;
#233985=CARTESIAN_POINT ( 'NONE',  ( -16.79270642812296543, 9.946244216949359895, -154.8389332785629904 ) ) ;
#234007=CARTESIAN_POINT ( 'NONE',  ( -17.73285935862607587, 10.85798180379782352, -144.2414381902258356 ) ) ;
#234782=ORIENTED_EDGE ( 'NONE', *, *, #222801, .F. ) ;
#234813=CARTESIAN_POINT ( 'NONE',  ( 16.27683809663750125, 9.350000000011137402, -143.2500000000000284 ) ) ;
#234826=( BOUNDED_SURFACE ( )  B_SPLINE_SURFACE ( 3, 2, ( 
 ( #24766, #140833, #219065 ),
 ( #160426, #181264, #65133 ),
 ( #161699, #239942, #120017 ),
 ( #199546, #204634, #20910 ) ),
 .UNSPECIFIED., .F., .F., .T. ) 
 B_SPLINE_SURFACE_WITH_KNOTS ( ( 4, 4 ),
 ( 3, 3 ),
 ( 0.0008258556059633754111, 0.0009616864997633037737 ),
 ( 0.000000000000000000, 1.000000000000000000 ),
 .UNSPECIFIED. ) 
 GEOMETRIC_REPRESENTATION_ITEM ( )  RATIONAL_B_SPLINE_SURFACE ( (
 ( 1.000000000000000000, 0.9152888060719425178, 1.000000000000000000),
 ( 1.000000000000000000, 0.9327727094138008601, 1.000000000000000000),
 ( 1.000000000000000000, 0.9369023509258477267, 1.000000000000000000),
 ( 1.000000000000000000, 0.9246339933864470284, 1.000000000000000000) ) ) 
 REPRESENTATION_ITEM ( '' )  SURFACE ( )  );
#234988=EDGE_CURVE ( 'NONE', #159239, #81429, #107463, .T. ) ;
#235111=CARTESIAN_POINT ( 'NONE',  ( -16.92989143108098560, 9.950000000011138823, -146.8824838747567298 ) ) ;
#235136=EDGE_CURVE ( 'NONE', #71322, #149588, #16098, .T. ) ;
#235197=( BOUNDED_SURFACE ( )  B_SPLINE_SURFACE ( 3, 2, ( 
 ( #161897, #235287, #253568 ),
 ( #121495, #136161, #234007 ),
 ( #124043, #201005, #83580 ),
 ( #196173, #180167, #160619 ) ),
 .UNSPECIFIED., .F., .F., .F. ) 
 B_SPLINE_SURFACE_WITH_KNOTS ( ( 4, 4 ),
 ( 3, 3 ),
 ( 5.727910411845712702, 5.983100554402350113 ),
 ( 0.000000000000000000, 1.000000000000000000 ),
 .UNSPECIFIED. ) 
 GEOMETRIC_REPRESENTATION_ITEM ( )  RATIONAL_B_SPLINE_SURFACE ( (
 ( 1.000000000000000000, 0.8946697475932060550, 1.000000000000000000),
 ( 1.000000000000000000, 0.9035312726220692259, 1.000000000000000000),
 ( 1.000000000000000000, 0.9104333467450208550, 1.000000000000000000),
 ( 1.000000000000000000, 0.9152888060719425178, 1.000000000000000000) ) ) 
 REPRESENTATION_ITEM ( '' )  SURFACE ( )  );
#235266=CARTESIAN_POINT ( 'NONE',  ( -16.92280123533721792, 9.950000000011137047, -154.6493676859139725 ) ) ;
#235287=CARTESIAN_POINT ( 'NONE',  ( -18.41431012584569160, 11.48747202921932065, -143.2267639868983622 ) ) ;
#235359=ORIENTED_EDGE ( 'NONE', *, *, #152381, .F. ) ;
#235391=CARTESIAN_POINT ( 'NONE',  ( -12.68215100488890812, 9.396630376328875656, -151.9070573928183592 ) ) ;
#235401=EDGE_CURVE ( 'NONE', #81429, #93783, #109708, .T. ) ;
#235657=DIRECTION ( 'NONE',  ( 0.000000000000000000, 0.000000000000000000, -1.000000000000000000 ) ) ;
#235851=CARTESIAN_POINT ( 'NONE',  ( -17.01825945287482966, 10.05000000001113847, -146.6500000000000341 ) ) ;
#235855=VERTEX_POINT ( 'NONE', #105526 ) ;
#235965=DIRECTION ( 'NONE',  ( 1.652117596168391700E-15, 1.000000000000000000, -0.000000000000000000 ) ) ;
#235993=DIRECTION ( 'NONE',  ( -0.8049926720990042694, -0.5932847527679310229, 0.000000000000000000 ) ) ;
#236138=EDGE_CURVE ( 'NONE', #118840, #70072, #252675, .T. ) ;
#236549=CARTESIAN_POINT ( 'NONE',  ( -16.93710578446422588, 9.950000000011137047, -154.5811960162002094 ) ) ;
#236599=EDGE_LOOP ( 'NONE', ( #124146, #56149 ) ) ;
#236693=AXIS2_PLACEMENT_3D ( 'NONE', #29709, #130040, #233035 ) ;
#236754=CARTESIAN_POINT ( 'NONE',  ( 18.39999999999999503, 11.75000000001113953, -146.6500000000000341 ) ) ;
#236858=CARTESIAN_POINT ( 'NONE',  ( 21.13736287352038445, 8.046642376395153562, -146.6500000000000341 ) ) ;
#236861=VERTEX_POINT ( 'NONE', #105571 ) ;
#237085=CARTESIAN_POINT ( 'NONE',  ( 20.73486653747088582, 7.250000000011182166, -146.6500000000000341 ) ) ;
#237091=DIRECTION ( 'NONE',  ( -1.000000000000000000, 0.000000000000000000, 0.000000000000000000 ) ) ;
#237337=COLOUR_RGB ( '', 0.31764706, 0.68627451, 0.89019608) ;
#237386=ADVANCED_FACE ( 'NONE', ( #103981 ), #126121, .F. ) ;
#237585=ORIENTED_EDGE ( 'NONE', *, *, #2726, .F. ) ;
#237617=ADVANCED_FACE ( 'NONE', ( #175559 ), #179405, .F. ) ;
#237958=CARTESIAN_POINT ( 'NONE',  ( -12.30589683808040924, 9.356746017089404788, -151.2033597213641940 ) ) ;
#237961=AXIS2_PLACEMENT_3D ( 'NONE', #51381, #167543, #25449 ) ;
#237986=CARTESIAN_POINT ( 'NONE',  ( -16.77683809663752257, 9.945835743215301505, -146.6639490191042228 ) ) ;
#238116=SHAPE_REPRESENTATION_RELATIONSHIP ( 'NONE' , 'NONE' ,  #63487, #132346 ) ;
#238543=CARTESIAN_POINT ( 'NONE',  ( 23.24999999999999645, 11.75000000001113953, -146.6500000000000341 ) ) ;
#238730=DIRECTION ( 'NONE',  ( -1.000000000000000000, 0.000000000000000000, 0.000000000000000000 ) ) ;
#238964=CARTESIAN_POINT ( 'NONE',  ( -16.81744102076749314, 9.950000000011142376, -146.6500000000000341 ) ) ;
#239129=DIRECTION ( 'NONE',  ( -0.000000000000000000, -0.000000000000000000, -1.000000000000000000 ) ) ;
#239580=DIRECTION ( 'NONE',  ( 1.000000000000000000, 0.000000000000000000, 0.000000000000000000 ) ) ;
#239616=ORIENTED_EDGE ( 'NONE', *, *, #147256, .T. ) ;
#239631=ORIENTED_EDGE ( 'NONE', *, *, #126868, .F. ) ;
#239788=LINE ( 'NONE', #212845, #167322 ) ;
#239897=LINE ( 'NONE', #199498, #108132 ) ;
#239904=DIRECTION ( 'NONE',  ( 0.000000000000000000, -1.000000000000000000, 0.000000000000000000 ) ) ;
#239942=CARTESIAN_POINT ( 'NONE',  ( -16.90202395485681919, 9.965944544562010066, -154.9030137212600096 ) ) ;
#240276=ORIENTED_EDGE ( 'NONE', *, *, #127837, .T. ) ;
#240416=LINE ( 'NONE', #124323, #29180 ) ;
#240429=EDGE_CURVE ( 'NONE', #209017, #252467, #216165, .T. ) ;
#240696=FILL_AREA_STYLE ('',( #42485 ) ) ;
#240864=CARTESIAN_POINT ( 'NONE',  ( 13.99999999999999822, 9.850000000011137402, -150.7500000000000284 ) ) ;
#240925=ORIENTED_EDGE ( 'NONE', *, *, #16628, .T. ) ;
#241178=ORIENTED_EDGE ( 'NONE', *, *, #44395, .T. ) ;
#241185=CARTESIAN_POINT ( 'NONE',  ( 23.24999999999999645, 8.822561741677553471, -146.6500000000000341 ) ) ;
#241416=( LENGTH_UNIT ( ) NAMED_UNIT ( * ) SI_UNIT ( .MILLI., .METRE. ) );
#241430=CARTESIAN_POINT ( 'NONE',  ( 13.22261339317536866, 9.436552840015581367, -149.1779554727603454 ) ) ;
#241444=CARTESIAN_POINT ( 'NONE',  ( -17.29838795458566025, 10.37154985795929818, -156.1047412826179368 ) ) ;
#241609=ORIENTED_EDGE ( 'NONE', *, *, #254431, .T. ) ;
#241746=DIRECTION ( 'NONE',  ( 1.000000000000000000, 0.000000000000000000, 0.000000000000000000 ) ) ;
#241819=CARTESIAN_POINT ( 'NONE',  ( -14.77538296656415362, 9.436662931810241517, -152.3230367322949235 ) ) ;
#241933=DIRECTION ( 'NONE',  ( -1.000000000000000000, 0.000000000000000000, 0.000000000000000000 ) ) ;
#242127=( BOUNDED_SURFACE ( )  B_SPLINE_SURFACE ( 3, 2, ( 
 ( #199763, #161919, #79759 ),
 ( #241444, #198449, #121513 ),
 ( #1522, #120241, #98033 ),
 ( #219292, #159348, #180190 ) ),
 .UNSPECIFIED., .F., .F., .F. ) 
 B_SPLINE_SURFACE_WITH_KNOTS ( ( 4, 4 ),
 ( 3, 3 ),
 ( 0.3000847527772392276, 0.5552748953338751958 ),
 ( 0.000000000000000000, 1.000000000000000000 ),
 .UNSPECIFIED. ) 
 GEOMETRIC_REPRESENTATION_ITEM ( )  RATIONAL_B_SPLINE_SURFACE ( (
 ( 1.000000000000000000, 0.9152888060719425178, 1.000000000000000000),
 ( 1.000000000000000000, 0.9104333467450189676, 1.000000000000000000),
 ( 1.000000000000000000, 0.9035312726220716684, 1.000000000000000000),
 ( 1.000000000000000000, 0.8946697475932030574, 1.000000000000000000) ) ) 
 REPRESENTATION_ITEM ( '' )  SURFACE ( )  );
#242208=CARTESIAN_POINT ( 'NONE',  ( -16.77683809663752257, 9.945835743215303282, -154.8360509808958057 ) ) ;
#242248=VERTEX_POINT ( 'NONE', #210067 ) ;
#242418=CARTESIAN_POINT ( 'NONE',  ( -16.87331047859649757, 9.950000000011138823, -154.8500000000000227 ) ) ;
#242423=EDGE_CURVE ( 'NONE', #242248, #39025, #239897, .T. ) ;
#242647=CARTESIAN_POINT ( 'NONE',  ( -17.05016517655648656, 9.950000000011138823, -146.6726979959938433 ) ) ;
#242677=( NAMED_UNIT ( * ) SI_UNIT ( $, .STERADIAN. ) SOLID_ANGLE_UNIT ( ) );
#242710=CARTESIAN_POINT ( 'NONE',  ( 20.09999999999999787, 9.750000000011137757, -143.2500000000000284 ) ) ;
#242791=DIRECTION ( 'NONE',  ( 0.7071067811865493491, 0.7071067811865456854, 0.000000000000000000 ) ) ;
#242803=CARTESIAN_POINT ( 'NONE',  ( -16.77308656112214180, 9.950000000011137047, -146.6501931917023001 ) ) ;
#242835=( BOUNDED_CURVE ( )  B_SPLINE_CURVE ( 3, ( #13043, #155131, #172134, #73030 ),
 .UNSPECIFIED., .F., .F. ) 
 B_SPLINE_CURVE_WITH_KNOTS ( ( 4, 4 ),
 ( 0.3000847527772381729, 0.5497968875596822569 ),
 .UNSPECIFIED. ) 
 CURVE ( )  GEOMETRIC_REPRESENTATION_ITEM ( )  RATIONAL_B_SPLINE_CURVE ( ( 1.000000000000000000, 0.9948104011409419911, 0.9948104011409419911, 1.000000000000000000 ) ) 
 REPRESENTATION_ITEM ( '' )  );
#243074=EDGE_CURVE ( 'NONE', #199629, #1028, #150201, .T. ) ;
#243120=EDGE_CURVE ( 'NONE', #103596, #45717, #244753, .T. ) ;
#243246=CARTESIAN_POINT ( 'NONE',  ( -16.87331047859651179, 9.950000000011142376, -146.6500000000000341 ) ) ;
#243294=CARTESIAN_POINT ( 'NONE',  ( 15.75000000000000000, 9.350000000011135626, -150.8657431672739619 ) ) ;
#243396=VECTOR ( 'NONE', #72142, 1000.000000000000000 ) ;
#243472=CARTESIAN_POINT ( 'NONE',  ( -16.80100914604134132, 9.943149094114721365, -154.8170441272876587 ) ) ;
#243533=CARTESIAN_POINT ( 'NONE',  ( -16.94180778212363592, 9.992443055743303049, -146.6041835705332517 ) ) ;
#243989=FACE_OUTER_BOUND ( 'NONE', #137253, .T. ) ;
#244086=CARTESIAN_POINT ( 'NONE',  ( -16.84981964351498007, 9.917318234109995245, -146.8696016140195013 ) ) ;
#244394=LINE ( 'NONE', #43642, #14414 ) ;
#244414=CARTESIAN_POINT ( 'NONE',  ( -16.81453046979149235, 9.939102281452070642, -146.7117265236030619 ) ) ;
#244439=CARTESIAN_POINT ( 'NONE',  ( -16.97683809663752186, 9.950000000011138823, -147.4023640181965220 ) ) ;
#244487=EDGE_LOOP ( 'NONE', ( #93912, #48567, #223960, #93856, #71721 ) ) ;
#244659=DIRECTION ( 'NONE',  ( 0.000000000000000000, 0.000000000000000000, 1.000000000000000000 ) ) ;
#244744=CARTESIAN_POINT ( 'NONE',  ( -16.80469485234342031, 9.942151663152193564, -154.8099668439312211 ) ) ;
#244753=( BOUNDED_CURVE ( )  B_SPLINE_CURVE ( 3, ( #192439, #149479, #67353, #229004 ),
 .UNSPECIFIED., .F., .F. ) 
 B_SPLINE_CURVE_WITH_KNOTS ( ( 4, 4 ),
 ( 0.000000000000000000, 1.570796326794896558 ),
 .UNSPECIFIED. ) 
 CURVE ( )  GEOMETRIC_REPRESENTATION_ITEM ( )  RATIONAL_B_SPLINE_CURVE ( ( 1.000000000000000000, 0.8047378541243649375, 0.8047378541243649375, 1.000000000000000000 ) ) 
 REPRESENTATION_ITEM ( '' )  );
#244877=CARTESIAN_POINT ( 'NONE',  ( -33.72168855820452649, 11.47316190337362585, -143.2500000000000284 ) ) ;
#245238=CARTESIAN_POINT ( 'NONE',  ( -17.04295772865466319, 10.02489942527108369, -146.6500000000000341 ) ) ;
#245293=DIRECTION ( 'NONE',  ( 1.000000000000000000, 0.000000000000000000, 0.000000000000000000 ) ) ;
#245388=EDGE_CURVE ( 'NONE', #225332, #199264, #195304, .T. ) ;
#245389=VECTOR ( 'NONE', #40118, 1000.000000000000000 ) ;
#245586=EDGE_LOOP ( 'NONE', ( #257472, #17125, #24239, #56610 ) ) ;
#245669=EDGE_CURVE ( 'NONE', #22565, #43985, #151968, .T. ) ;
#245718=DIRECTION ( 'NONE',  ( -1.020425574104004196E-15, 0.000000000000000000, 1.000000000000000000 ) ) ;
#245825=CARTESIAN_POINT ( 'NONE',  ( -20.65000000000000568, 7.250000000011138646, -146.6500000000000341 ) ) ;
#245904=ORIENTED_EDGE ( 'NONE', *, *, #187254, .T. ) ;
#246377=EDGE_CURVE ( 'NONE', #83264, #220835, #72768, .T. ) ;
#247075=LINE ( 'NONE', #68466, #120214 ) ;
#247173=ADVANCED_FACE ( 'NONE', ( #232171 ), #194339, .F. ) ;
#247301=AXIS2_PLACEMENT_3D ( 'NONE', #97564, #256610, #42756 ) ;
#247572=CARTESIAN_POINT ( 'NONE',  ( 20.73486653747088582, 7.250000000011182166, -143.2500000000000284 ) ) ;
#247585=DIRECTION ( 'NONE',  ( -0.7071067811865463515, -0.7071067811865487940, 7.587431340288849180E-16 ) ) ;
#247820=CARTESIAN_POINT ( 'NONE',  ( -16.87331047859651179, 9.950000000011142376, -146.6500000000000341 ) ) ;
#248024=ORIENTED_EDGE ( 'NONE', *, *, #95962, .F. ) ;
#248072=DIRECTION ( 'NONE',  ( 1.000000000000000000, 0.000000000000000000, -0.000000000000000000 ) ) ;
#248174=CARTESIAN_POINT ( 'NONE',  ( -18.40000000000000213, 5.650000000011139001, -158.2500000000000284 ) ) ;
#248183=ORIENTED_EDGE ( 'NONE', *, *, #149992, .F. ) ;
#248213=EDGE_LOOP ( 'NONE', ( #173641, #251462, #155398, #254154 ) ) ;
#248470=ORIENTED_EDGE ( 'NONE', *, *, #243120, .T. ) ;
#248882=APPLICATION_CONTEXT ( 'automotive_design' ) ;
#249157=CARTESIAN_POINT ( 'NONE',  ( -14.00000000000000178, 9.850000000011133849, -150.7500000000000284 ) ) ;
#249237=CARTESIAN_POINT ( 'NONE',  ( -16.94445028196807002, 9.992063609708893068, -154.8926698215815634 ) ) ;
#249271=ORIENTED_EDGE ( 'NONE', *, *, #213404, .F. ) ;
#249279=CARTESIAN_POINT ( 'NONE',  ( -16.87665923198281348, 9.950000000011138823, -154.8500000000000227 ) ) ;
#249317=CIRCLE ( 'NONE', #36960, 14.30833333333333890 ) ;
#249893=CARTESIAN_POINT ( 'NONE',  ( 20.99999999999999645, 9.750000000011137757, -146.6500000000000341 ) ) ;
#250013=ORIENTED_EDGE ( 'NONE', *, *, #212637, .F. ) ;
#250016=ADVANCED_FACE ( 'NONE', ( #82375 ), #101941, .F. ) ;
#250060=CARTESIAN_POINT ( 'NONE',  ( -14.56556274378147542, 9.446557523083688679, -149.0899419543459601 ) ) ;
#250207=VECTOR ( 'NONE', #77391, 1000.000000000000000 ) ;
#250341=CARTESIAN_POINT ( 'NONE',  ( -16.78270389226384651, 9.947372616628161524, -154.8412070369114701 ) ) ;
#250428=EDGE_CURVE ( 'NONE', #203266, #212672, #200765, .T. ) ;
#250456=LINE ( 'NONE', #194369, #35437 ) ;
#250587=CARTESIAN_POINT ( 'NONE',  ( -16.94107738177414291, 10.01423928514777373, -154.9500000000000455 ) ) ;
#250861=DIRECTION ( 'NONE',  ( -0.000000000000000000, -0.000000000000000000, -1.000000000000000000 ) ) ;
#250880=ORIENTED_EDGE ( 'NONE', *, *, #145596, .F. ) ;
#251041=EDGE_CURVE ( 'NONE', #225791, #56249, #95594, .T. ) ;
#251109=CARTESIAN_POINT ( 'NONE',  ( -16.97683809663752186, 9.950000000011137047, -147.4023640181965220 ) ) ;
#251114=PLANE ( 'NONE',  #97915 ) ;
#251204=VECTOR ( 'NONE', #141204, 1000.000000000000000 ) ;
#251326=CARTESIAN_POINT ( 'NONE',  ( -13.12432614554023047, 9.430764995433476017, -149.2305373947504847 ) ) ;
#251377=DIRECTION ( 'NONE',  ( 1.000000000000000000, 0.000000000000000000, 0.000000000000000000 ) ) ;
#251420=DIRECTION ( 'NONE',  ( 1.000000000000000000, 1.186688945009010077E-16, 0.000000000000000000 ) ) ;
#251462=ORIENTED_EDGE ( 'NONE', *, *, #163565, .T. ) ;
#251769=CARTESIAN_POINT ( 'NONE',  ( -21.65000000000000213, 7.250000000011138646, -146.6500000000000341 ) ) ;
#251913=CARTESIAN_POINT ( 'NONE',  ( -16.94107738177414291, 10.01423928514777373, -154.9500000000000455 ) ) ;
#252467=VERTEX_POINT ( 'NONE', #244439 ) ;
#252675=B_SPLINE_CURVE_WITH_KNOTS ( 'NONE', 3,
 ( #43991, #7423, #102653, #227759, #222602, #223896, #46541, #28321, #23174, #244744, #243472, #66124, #83076, #183508 ),
 .UNSPECIFIED., .F., .F.,
 ( 4, 2, 2, 2, 2, 2, 4 ),
 ( 0.000000000000000000, 0.0003823333598417661934, 0.0005735000397626486938, 0.0006690833797230898898, 0.0007168750497033118431, 0.0007407708846934227655, 0.0007646667196835337963 ),
 .UNSPECIFIED. ) ;
#252761=AXIS2_PLACEMENT_3D ( 'NONE', #65249, #24873, #106933 ) ;
#253112=CARTESIAN_POINT ( 'NONE',  ( -18.40000000000000213, 11.48667500176882861, -158.2500000000000284 ) ) ;
#253195=CARTESIAN_POINT ( 'NONE',  ( -21.64999999999999858, 10.05000000001113847, -146.6500000000000341 ) ) ;
#253233=DIRECTION ( 'NONE',  ( -1.000000000000000000, 0.000000000000000000, 0.000000000000000000 ) ) ;
#253461=CARTESIAN_POINT ( 'NONE',  ( -17.01473183483382812, 9.950000000011137047, -146.7500000000000284 ) ) ;
#253543=CARTESIAN_POINT ( 'NONE',  ( -16.87333278164157946, 9.882609784590092872, -154.3668321938465624 ) ) ;
#253568=CARTESIAN_POINT ( 'NONE',  ( -18.37013991200266005, 11.49974761622312691, -143.2069769894829108 ) ) ;
#253663=CARTESIAN_POINT ( 'NONE',  ( -12.26136940704872025, 9.351403174152810749, -150.9795304368385302 ) ) ;
#253978=CIRCLE ( 'NONE', #233361, 0.09999999999999602263 ) ;
#254065=DIRECTION ( 'NONE',  ( -1.020425574104004196E-15, -1.210927747993693964E-31, -1.000000000000000000 ) ) ;
#254154=ORIENTED_EDGE ( 'NONE', *, *, #236138, .T. ) ;
#254421=CARTESIAN_POINT ( 'NONE',  ( -16.93433913041102912, 10.00597842153509376, -154.9353654273951975 ) ) ;
#254431=EDGE_CURVE ( 'NONE', #49221, #10139, #24486, .T. ) ;
#254441=ORIENTED_EDGE ( 'NONE', *, *, #173443, .T. ) ;
#254604=CARTESIAN_POINT ( 'NONE',  ( -16.87331047859649757, 9.950000000011138823, -154.8500000000000227 ) ) ;
#254762=CARTESIAN_POINT ( 'NONE',  ( -23.25000000000000355, 11.75000000001113953, -158.2500000000000284 ) ) ;
#254787=CARTESIAN_POINT ( 'NONE',  ( -16.80621392010912629, 9.942202577518866491, -154.8104080345828777 ) ) ;
#254838=VERTEX_POINT ( 'NONE', #113719 ) ;
#254900=CARTESIAN_POINT ( 'NONE',  ( -12.25000000000000178, 9.350000000011139178, -150.7500000000000284 ) ) ;
#254979=CARTESIAN_POINT ( 'NONE',  ( -12.25000000000000178, 9.850000000011133849, -150.7500000000000284 ) ) ;
#255072=ORIENTED_EDGE ( 'NONE', *, *, #54134, .T. ) ;
#255402=ORIENTED_EDGE ( 'NONE', *, *, #130205, .T. ) ;
#255477=DIRECTION ( 'NONE',  ( 0.000000000000000000, 0.000000000000000000, -1.000000000000000000 ) ) ;
#255513=AXIS2_PLACEMENT_3D ( 'NONE', #164562, #242791, #61598 ) ;
#255778=LINE ( 'NONE', #15960, #116799 ) ;
#255907=DIRECTION ( 'NONE',  ( 1.000000000000000000, -0.000000000000000000, -0.000000000000000000 ) ) ;
#255927=LINE ( 'NONE', #77329, #40868 ) ;
#256003=CARTESIAN_POINT ( 'NONE',  ( -16.87036670365548474, 9.989418819312801290, -154.9795601173020714 ) ) ;
#256073=VERTEX_POINT ( 'NONE', #47666 ) ;
#256137=CARTESIAN_POINT ( 'NONE',  ( 18.54999999999999716, 8.750000000011182166, -154.8500000000000227 ) ) ;
#256162=VECTOR ( 'NONE', #28532, 1000.000000000000000 ) ;
#256250=B_SPLINE_CURVE_WITH_KNOTS ( 'NONE', 3,
 ( #115155, #194717, #95583, #218082, #235111, #116447, #197255, #58997, #17347, #238964 ),
 .UNSPECIFIED., .F., .F.,
 ( 4, 2, 2, 2, 4 ),
 ( 0.000000000000000000, 0.0003916577441626726262, 0.0005874866162440096169, 0.0006854010522846797114, 0.0007833154883253498060 ),
 .UNSPECIFIED. ) ;
#256460=CARTESIAN_POINT ( 'NONE',  ( -21.64999999999999858, 10.05000000001113847, -154.8500000000000227 ) ) ;
#256565=ORIENTED_EDGE ( 'NONE', *, *, #144182, .T. ) ;
#256610=DIRECTION ( 'NONE',  ( 1.186688945009009831E-16, -1.000000000000000000, 0.000000000000000000 ) ) ;
#256785=CARTESIAN_POINT ( 'NONE',  ( 18.54999999999999716, 9.950000000011153034, -146.6499999999999773 ) ) ;
#256949=ORIENTED_EDGE ( 'NONE', *, *, #96111, .T. ) ;
#256999=VECTOR ( 'NONE', #66113, 1000.000000000000000 ) ;
#257218=ADVANCED_FACE ( 'NONE', ( #21623 ), #39922, .T. ) ;
#257287=CARTESIAN_POINT ( 'NONE',  ( -18.34374000495059676, 11.47316190337362940, -158.2500000000000284 ) ) ;
#257299=( BOUNDED_SURFACE ( )  B_SPLINE_SURFACE ( 3, 2, ( 
 ( #232243, #75725, #130542 ),
 ( #213939, #172295, #54845 ),
 ( #52276, #35343, #91432 ),
 ( #11914, #53586, #13182 ) ),
 .UNSPECIFIED., .F., .F., .F. ) 
 B_SPLINE_SURFACE_WITH_KNOTS ( ( 4, 4 ),
 ( 3, 3 ),
 ( 0.0008258556059633777964, 0.0009616864997632713560 ),
 ( 0.000000000000000000, 1.000000000000000000 ),
 .UNSPECIFIED. ) 
 GEOMETRIC_REPRESENTATION_ITEM ( )  RATIONAL_B_SPLINE_SURFACE ( (
 ( 1.000000000000000000, 0.9152888060719425178, 1.000000000000000000),
 ( 1.000000000000000000, 0.9327727094137988617, 1.000000000000000000),
 ( 1.000000000000000000, 0.9369023509258489479, 1.000000000000000000),
 ( 1.000000000000000000, 0.9246339933864502481, 1.000000000000000000) ) ) 
 REPRESENTATION_ITEM ( '' )  SURFACE ( )  );
#257472=ORIENTED_EDGE ( 'NONE', *, *, #170993, .F. ) ;
#257921=ORIENTED_EDGE ( 'NONE', *, *, #135947, .T. ) ;
ENDSEC;
END-ISO-10303-21;
